ISO-10303-21;
HEADER;
FILE_DESCRIPTION (('STEP AP214'),
    '1' );
FILE_NAME ('510 Connector Pin.step',
    '2026-10-05T22:38:29',
    ( '' ),
    ( '' ),
    'SwSTEP 2.0',
    'SolidWorks 2020',
    '' );
FILE_SCHEMA (( 'AUTOMOTIVE_DESIGN' ));
ENDSEC;

DATA;
#59=CARTESIAN_POINT ( 'NONE',  ( 4.808535432091000317, -0.4767679613171000308, 1.182990937922999919 ) ) ;
#69=CARTESIAN_POINT ( 'NONE',  ( 4.719609839682791907, -0.1963495408493605987, -1.500000000000000444 ) ) ;
#94=CARTESIAN_POINT ( 'NONE',  ( 0.7000000000000000666, 0.000000000000000000, 0.000000000000000000 ) ) ;
#95=VERTEX_POINT ( 'NONE', #41621 ) ;
#97=EDGE_LOOP ( 'NONE', ( #29437, #64562 ) ) ;
#127=CARTESIAN_POINT ( 'NONE',  ( 4.399793616306585164, -0.6172922141386431027, -0.9509182009922042544 ) ) ;
#143=CARTESIAN_POINT ( 'NONE',  ( 5.807487603146999966, -1.101608967510000037, 0.4118716830840000176 ) ) ;
#146=VERTEX_POINT ( 'NONE', #46530 ) ;
#185=CARTESIAN_POINT ( 'NONE',  ( 4.658558767843999249, -0.5257635793736999963, -1.466092528140000129 ) ) ;
#218=CARTESIAN_POINT ( 'NONE',  ( 6.627690453616000177, -1.117491691666000042, 0.8211442336051000268 ) ) ;
#221=EDGE_LOOP ( 'NONE', ( #55907, #18470, #68764, #30688 ) ) ;
#226=CARTESIAN_POINT ( 'NONE',  ( 0.7000000000000000666, 0.5773502691895999739, -1.000000000000000000 ) ) ;
#240=CARTESIAN_POINT ( 'NONE',  ( 5.982073283530000118, -0.8842068839782000200, 1.351115652313999771 ) ) ;
#301=CARTESIAN_POINT ( 'NONE',  ( 6.928706320015000308, -0.2869491282519000541, -1.095445449434000018 ) ) ;
#343=CARTESIAN_POINT ( 'NONE',  ( 5.752943173017458278, 1.199500263597271577, -0.9218200799623702535 ) ) ;
#362=DIRECTION ( 'NONE',  ( 0.000000000000000000, -1.000000000000000000, 0.000000000000000000 ) ) ;
#368=LINE ( 'NONE', #31851, #12349 ) ;
#380=CARTESIAN_POINT ( 'NONE',  ( 5.028782850970884510, 0.9602633891249825471, -0.7171280660100972648 ) ) ;
#402=CARTESIAN_POINT ( 'NONE',  ( 7.199141827028999963, 0.000000000000000000, 0.000000000000000000 ) ) ;
#415=CARTESIAN_POINT ( 'NONE',  ( 4.677943173015960632, -0.9218200799623716968, -1.199500263597270910 ) ) ;
#423=EDGE_LOOP ( 'NONE', ( #35216, #41530, #64033, #16512, #37170, #10912, #48215, #947, #69122, #9098 ) ) ;
#426=VERTEX_POINT ( 'NONE', #5845 ) ;
#428=CARTESIAN_POINT ( 'NONE',  ( 6.180771831090410728, 0.3343430079570269275, 1.082181004987261330 ) ) ;
#454=CARTESIAN_POINT ( 'NONE',  ( 4.446647932087000044, 1.441877299643999910, 0.3432711633658000472 ) ) ;
#464=CYLINDRICAL_SURFACE ( 'NONE', #11206, 1.500000000000000000 ) ;
#488=CARTESIAN_POINT ( 'NONE',  ( 5.375631947951000633, -0.1057711097905999903, -1.318062398728999884 ) ) ;
#531=CARTESIAN_POINT ( 'NONE',  ( 5.332217238860999409, 0.4341136435772000035, 1.348325027692000022 ) ) ;
#543=CARTESIAN_POINT ( 'NONE',  ( 4.587940964153251144, -1.500000000000001332, 0.3220548830679713093 ) ) ;
#544=CIRCLE ( 'NONE', #61931, 0.5999999999999999778 ) ;
#588=CARTESIAN_POINT ( 'NONE',  ( 5.629173046212000209, -1.056937757944000023, -1.220746830110999825 ) ) ;
#632=CARTESIAN_POINT ( 'NONE',  ( 5.077371418665322267, -0.3835488334464972615, 1.315173458188629851 ) ) ;
#651=CARTESIAN_POINT ( 'NONE',  ( 6.895498187670000334, -0.7063073661229000155, -0.8851390247125999755 ) ) ;
#690=ORIENTED_EDGE ( 'NONE', *, *, #61029, .F. ) ;
#728=CARTESIAN_POINT ( 'NONE',  ( 4.759810628746807382, -0.7637421492518075006, 0.9236198983835054444 ) ) ;
#775=CARTESIAN_POINT ( 'NONE',  ( 6.423150728792507813, -0.4364103388565075958, -1.045044225101665614 ) ) ;
#803=CARTESIAN_POINT ( 'NONE',  ( 4.686986683301000767, -0.8504805407472000311, 1.028515646795000071 ) ) ;
#820=CARTESIAN_POINT ( 'NONE',  ( 4.399761055266754539, -0.1241639754006147178, -1.193569193835689379 ) ) ;
#835=CARTESIAN_POINT ( 'NONE',  ( 6.686404257991999778, -0.8351886993729999986, 1.025064727650000007 ) ) ;
#880=CARTESIAN_POINT ( 'NONE',  ( 4.795397656733999092, 1.527828479674999906, -0.3026462966785000153 ) ) ;
#912=AXIS2_PLACEMENT_3D ( 'NONE', #56306, #8412, #34650 ) ;
#916=MECHANICAL_DESIGN_GEOMETRIC_PRESENTATION_REPRESENTATION('',(#29982),#21023);
#936=CARTESIAN_POINT ( 'NONE',  ( 5.751874906802000531, 1.422967556274000067, 0.3628923349178999613 ) ) ;
#942=CARTESIAN_POINT ( 'NONE',  ( 6.115443173016667622, -1.500000000000000222, -0.1963495408493622085 ) ) ;
#947=ORIENTED_EDGE ( 'NONE', *, *, #10087, .F. ) ;
#971=CARTESIAN_POINT ( 'NONE',  ( 5.846693173017501799, 1.310679582531385501, 0.7554284705563518720 ) ) ;
#979=EDGE_CURVE ( 'NONE', #25079, #67571, #55510, .T. ) ;
#999=CARTESIAN_POINT ( 'NONE',  ( 7.327076482695999537, -0.8753148192162999441, 0.8932045635694000341 ) ) ;
#1014=VECTOR ( 'NONE', #43655, 1000.000000000000114 ) ;
#1027=CARTESIAN_POINT ( 'NONE',  ( 5.719609839683332808, -0.1963495408493605987, -1.500000000000000444 ) ) ;
#1068=EDGE_LOOP ( 'NONE', ( #44039, #31133, #6167, #22308 ) ) ;
#1100=DIRECTION ( 'NONE',  ( 0.000000000000000000, 0.000000000000000000, -1.000000000000000000 ) ) ;
#1112=CARTESIAN_POINT ( 'NONE',  ( 6.587956561560666557, -1.500000000000001332, 0.3217608788839342315 ) ) ;
#1122=CARTESIAN_POINT ( 'NONE',  ( 6.229247610630833876, -0.3449401851437640110, 1.078764845586133392 ) ) ;
#1152=CARTESIAN_POINT ( 'NONE',  ( 4.740781127745999690, -1.306963758498000061, 0.2701982545766000166 ) ) ;
#1159=CARTESIAN_POINT ( 'NONE',  ( 5.605026506349999771, -1.500000000000000000, 0.000000000000000000 ) ) ;
#1183=CARTESIAN_POINT ( 'NONE',  ( 6.506620200880000482, 0.8089969479913999839, 1.225571816066999942 ) ) ;
#1212=CARTESIAN_POINT ( 'NONE',  ( 4.877943173016666023, 0.9218200799623692543, 1.199500263597272687 ) ) ;
#1222=CARTESIAN_POINT ( 'NONE',  ( 5.389233442565000587, -0.5479625777084999871, 1.274769677192999939 ) ) ;
#1276=CARTESIAN_POINT ( 'NONE',  ( 6.284559201231999737, 1.526675769738000010, -0.5259243426933000176 ) ) ;
#1320=VECTOR ( 'NONE', #52571, 1000.000000000000000 ) ;
#1335=CARTESIAN_POINT ( 'NONE',  ( 7.326949057234999785, 0.08117426202284000469, 1.366388098755000113 ) ) ;
#1341=B_SPLINE_CURVE_WITH_KNOTS ( 'NONE', 3,
 ( #64302, #54167, #38789, #32176, #38439, #5581, #1381, #6267, #54521, #59413, #16420, #37748, #26924, #343, #64988, #21660, #59761, #49619 ),
 .UNSPECIFIED., .F., .F.,
 ( 4, 2, 2, 2, 2, 2, 2, 2, 4 ),
 ( 0.000000000000000000, 0.1250000000000000000, 0.2500000000000000000, 0.3750000000000000000, 0.5000000000000000000, 0.6250000000000000000, 0.7500000000000000000, 0.8750000000000000000, 1.000000000000000000 ),
 .UNSPECIFIED. ) ;
#1381=CARTESIAN_POINT ( 'NONE',  ( 5.638359839683665165, -0.7554284705563483193, -1.310679582531387721 ) ) ;
#1433=CARTESIAN_POINT ( 'NONE',  ( 6.903516731156273067, -1.060941250248529810, 0.7957428194428121104 ) ) ;
#1481=VECTOR ( 'NONE', #30903, 1000.000000000000000 ) ;
#1495=CARTESIAN_POINT ( 'NONE',  ( 4.550764323399000055, 1.072805779648999813, -0.5080389213338001309 ) ) ;
#1523=CARTESIAN_POINT ( 'NONE',  ( 6.326836143768000298, 1.551976682437999910, -0.4457619964912000188 ) ) ;
#1621=CARTESIAN_POINT ( 'NONE',  ( 6.435802160082999990, 0.003195320017092000316, 1.614721372341000105 ) ) ;
#1665=CARTESIAN_POINT ( 'NONE',  ( 6.691040091391770694, -0.7154887884274937493, -1.338493503189307487 ) ) ;
#1707=AXIS2_PLACEMENT_3D ( 'NONE', #13473, #45284, #49829 ) ;
#1759=B_SPLINE_SURFACE_WITH_KNOTS ( 'NONE', 3, 3, ( 
 ( #46830, #36334, #57649, #20946, #35315, #31103, #8736, #51381, #35657, #3480, #40892, #56971, #30410, #51722, #3817, #25154, #67793, #19914, #10443 ),
 ( #6226, #32134, #69172, #11472, #1335, #27566, #53787, #38046, #33160, #49228, #22310, #32472, #54477, #21620, #54127, #48894, #17062, #26884, #21282 ),
 ( #5883, #43303, #999, #64610, #32812, #37363, #59034, #42955, #43651, #38394, #37708, #63582, #64947, #48199, #26539, #37028, #16378, #59719, #31783 ),
 ( #11819, #58340, #6578, #16033, #27918, #27222, #42279, #11137, #53447, #48547, #15697, #63922, #301, #651, #53101, #5199, #47865, #42612, #21964 ) ),
 .UNSPECIFIED., .F., .F., .F.,
 ( 4, 4 ),
 ( 4, 1, 1, 1, 1, 1, 1, 1, 1, 1, 1, 1, 1, 1, 1, 1, 4 ),
 ( 0.1425182627899000132, 1.026369452518000047 ),
 ( 0.6640607743075999103, 0.6854686661408999626, 0.7068765579742000149, 0.7282844498075999873, 0.7496923416409000396, 0.7711002334743000119, 0.7925081253075999532, 0.8139160171409000055, 0.8353239089742999779, 0.8567318008076000302, 0.8781396926410000026, 0.8995475844743000549, 0.9209554763077000272, 0.9423633681409999685, 0.9637712599743000208, 0.9851791518076999932, 1.006587043640999823 ),
 .UNSPECIFIED. ) ;
#1786=LINE ( 'NONE', #50719, #5342 ) ;
#1813=CARTESIAN_POINT ( 'NONE',  ( 6.600895253773083837, 1.094225353004803170, 0.2934724196684175279 ) ) ;
#1843=CARTESIAN_POINT ( 'NONE',  ( 5.171136683305999071, -0.5839666677625000579, 1.090217988517000025 ) ) ;
#1851=CARTESIAN_POINT ( 'NONE',  ( 4.529188755291665203, -1.439555872821473681, 0.4868043516139976545 ) ) ;
#1876=CARTESIAN_POINT ( 'NONE',  ( 5.095019251604999688, -0.7389799844016000652, 1.268943043503000023 ) ) ;
#1892=DIRECTION ( 'NONE',  ( 0.000000000000000000, 0.000000000000000000, -1.000000000000000000 ) ) ;
#1972=CARTESIAN_POINT ( 'NONE',  ( 5.846035669131000034, -1.131660731475000015, -0.3201946116248999830 ) ) ;
#2054=VERTEX_POINT ( 'NONE', #61175 ) ;
#2083=ORIENTED_EDGE ( 'NONE', *, *, #54861, .T. ) ;
#2193=CARTESIAN_POINT ( 'NONE',  ( 4.170446217910000364, -0.9708739270978999913, -1.205883038339000235 ) ) ;
#2199=PRODUCT_DEFINITION ( 'UNKNOWN', '', #31816, #58350 ) ;
#2224=CARTESIAN_POINT ( 'NONE',  ( 6.002477004709999342, 0.8716839254852999375, 1.181818379215999970 ) ) ;
#2232=CARTESIAN_POINT ( 'NONE',  ( 7.400000000000000355, 0.000000000000000000, 0.000000000000000000 ) ) ;
#2311=CARTESIAN_POINT ( 'NONE',  ( 6.148521586833000541, 0.6981053669911999604, 0.9464826977047000600 ) ) ;
#2353=CARTESIAN_POINT ( 'NONE',  ( 6.764778664328501279, 0.6406565617180175476, -1.375763741981867794 ) ) ;
#2358=VERTEX_POINT ( 'NONE', #55760 ) ;
#2408=CYLINDRICAL_SURFACE ( 'NONE', #68991, 1.500000000000000000 ) ;
#2421=CARTESIAN_POINT ( 'NONE',  ( 6.513359839683332098, -1.310679582531389276, 0.7554284705563443225 ) ) ;
#2447=DIRECTION ( 'NONE',  ( 0.000000000000000000, -1.000000000000000000, 0.000000000000000000 ) ) ;
#2471=LINE ( 'NONE', #35333, #23027 ) ;
#2472=FACE_OUTER_BOUND ( 'NONE', #39066, .T. ) ;
#2555=CARTESIAN_POINT ( 'NONE',  ( 5.044604931988000196, 0.1454693244516999939, 1.365796648849999961 ) ) ;
#2566=DIRECTION ( 'NONE',  ( 0.000000000000000000, 1.000000000000000000, 0.000000000000000000 ) ) ;
#2596=DIRECTION ( 'NONE',  ( 0.000000000000000000, 0.000000000000000000, -1.000000000000000000 ) ) ;
#2651=CARTESIAN_POINT ( 'NONE',  ( 6.731620200880000127, 0.7284491026353999699, 1.103547660897999938 ) ) ;
#2771=CARTESIAN_POINT ( 'NONE',  ( 5.342753212293000153, 1.434852097279999850, 0.6058508543602000307 ) ) ;
#2800=CARTESIAN_POINT ( 'NONE',  ( 5.329623228227332810, 1.445318020077273724, 0.4634605740919916506 ) ) ;
#2878=ADVANCED_FACE ( 'NONE', ( #51962 ), #15259, .F. ) ;
#2889=CARTESIAN_POINT ( 'NONE',  ( 1.700000000000000178, 0.000000000000000000, 0.000000000000000000 ) ) ;
#2903=CARTESIAN_POINT ( 'NONE',  ( 6.055026506350000837, -1.500000000000000000, 0.000000000000000000 ) ) ;
#2915=CARTESIAN_POINT ( 'NONE',  ( 6.899999438051000133, 0.5526611926744998682, 1.394476821647000042 ) ) ;
#2968=ORIENTED_EDGE ( 'NONE', *, *, #31098, .F. ) ;
#2990=CARTESIAN_POINT ( 'NONE',  ( 6.249350226066000324, -0.6943539861719999484, 0.9492381903959000722 ) ) ;
#3008=DIRECTION ( 'NONE',  ( 0.000000000000000000, -1.000000000000000000, 0.000000000000000000 ) ) ;
#3052=CARTESIAN_POINT ( 'NONE',  ( 7.272653897099000453, -0.7925871808662000584, 0.8087861320687000921 ) ) ;
#3067=CARTESIAN_POINT ( 'NONE',  ( 5.221693173016666023, 0.7554284705563509839, -1.310679582531386167 ) ) ;
#3091=DIRECTION ( 'NONE',  ( 1.000000000000000000, 0.000000000000000000, 0.000000000000000000 ) ) ;
#3097=CARTESIAN_POINT ( 'NONE',  ( 5.002606837613999602, -0.4199405305951999789, 1.440017343911000003 ) ) ;
#3107=CARTESIAN_POINT ( 'NONE',  ( 6.440443173016666911, -0.1963495408493673156, 1.499999999999999556 ) ) ;
#3150=VERTEX_POINT ( 'NONE', #61011 ) ;
#3192=ADVANCED_FACE ( 'NONE', ( #7181 ), #6830, .T. ) ;
#3193=FACE_OUTER_BOUND ( 'NONE', #20944, .T. ) ;
#3220=CARTESIAN_POINT ( 'NONE',  ( 4.582870291988999867, -1.595997307511999752, 0.3299522913273999492 ) ) ;
#3334=CARTESIAN_POINT ( 'NONE',  ( 6.479548602795000889, -0.7569293636342000475, -1.084220404132000048 ) ) ;
#3376=CARTESIAN_POINT ( 'NONE',  ( -0.2999999999999999889, 0.5773502691895999739, 1.000000000000000000 ) ) ;
#3397=EDGE_CURVE ( 'NONE', #47471, #13866, #67900, .T. ) ;
#3401=EDGE_CURVE ( 'NONE', #24359, #44723, #27760, .T. ) ;
#3464=EDGE_LOOP ( 'NONE', ( #48545, #53593, #31926, #6711 ) ) ;
#3480=CARTESIAN_POINT ( 'NONE',  ( 7.227197234740000198, 1.247817563501999905, -0.8087676081403000206 ) ) ;
#3576=CARTESIAN_POINT ( 'NONE',  ( 7.077542425583873253, -1.465994342824544899E-06, -1.322443989608400816 ) ) ;
#3590=FACE_OUTER_BOUND ( 'NONE', #60039, .T. ) ;
#3594=ORIENTED_EDGE ( 'NONE', *, *, #41270, .F. ) ;
#3610=ORIENTED_EDGE ( 'NONE', *, *, #5918, .F. ) ;
#3656=CARTESIAN_POINT ( 'NONE',  ( 6.210802160082999457, 0.002327316029692000007, 1.176084684120999979 ) ) ;
#3687=ORIENTED_EDGE ( 'NONE', *, *, #12236, .F. ) ;
#3698=CARTESIAN_POINT ( 'NONE',  ( 5.188359839683666763, -0.7554284705563480973, -1.310679582531387277 ) ) ;
#3714=AXIS2_PLACEMENT_3D ( 'NONE', #55751, #2596, #362 ) ;
#3750=VERTEX_POINT ( 'NONE', #19655 ) ;
#3806=CARTESIAN_POINT ( 'NONE',  ( 7.156776345353000224, 1.243223188895000053, 2.274921040069000118E-10 ) ) ;
#3817=CARTESIAN_POINT ( 'NONE',  ( 7.061156573014000237, -1.318960494382000137, -0.6866539737626000672 ) ) ;
#3836=CARTESIAN_POINT ( 'NONE',  ( 6.562102968646999379, -1.381912473529000041, 0.6877288610791999490 ) ) ;
#3856=ORIENTED_EDGE ( 'NONE', *, *, #26270, .T. ) ;
#3889=DIRECTION ( 'NONE',  ( 0.000000000000000000, 0.9999503185633161761, 0.009967968956736161443 ) ) ;
#3918=CARTESIAN_POINT ( 'NONE',  ( 4.592741125323000162, 1.103414028882999887, 0.2634071631652999956 ) ) ;
#3937=CARTESIAN_POINT ( 'NONE',  ( 6.569697510850818212, -1.499768286218591706, -0.2711207260315494083 ) ) ;
#3998=CARTESIAN_POINT ( 'NONE',  ( 6.311630799317000218, -1.121550593885000113, 0.3539842735925000095 ) ) ;
#4008=CARTESIAN_POINT ( 'NONE',  ( 5.745207029897000162, -0.6440133831468000114, 0.9840870706126000345 ) ) ;
#4041=CARTESIAN_POINT ( 'NONE',  ( 5.334193173017583334, 1.460959015002474048, -0.3926218265389178064 ) ) ;
#4073=CARTESIAN_POINT ( 'NONE',  ( 7.027657817496000270, 1.230545047785000179, 0.3267465519018999953 ) ) ;
#4099=AXIS2_PLACEMENT_3D ( 'NONE', #53786, #37027, #42954 ) ;
#4151=CARTESIAN_POINT ( 'NONE',  ( 7.178932123752673533, 1.128209471082204374, 0.5373459335455109676 ) ) ;
#4167=CARTESIAN_POINT ( 'NONE',  ( 5.555026506349999948, -1.500000000000000000, 0.000000000000000000 ) ) ;
#4177=CARTESIAN_POINT ( 'NONE',  ( 0.7000000000000000666, 1.154700538379000108, 0.000000000000000000 ) ) ;
#4187=B_SPLINE_CURVE_WITH_KNOTS ( 'NONE', 3,
 ( #62360, #24274, #35797, #25644, #30550, #8883, #14479, #57447, #4310, #46637, #56784, #8536 ),
 .UNSPECIFIED., .F., .F.,
 ( 4, 2, 2, 2, 2, 4 ),
 ( 0.000000000000000000, 0.2500000000000000555, 0.3750000000000001110, 0.5000000000000001110, 0.7500000000000000000, 1.000000000000000000 ),
 .UNSPECIFIED. ) ;
#4221=CARTESIAN_POINT ( 'NONE',  ( 7.062379262093081422, 0.1858842090091465671, 1.343634368969766957 ) ) ;
#4233=ORIENTED_EDGE ( 'NONE', *, *, #31453, .T. ) ;
#4268=CARTESIAN_POINT ( 'NONE',  ( 5.116422932093001030, 1.142727098684000131, -0.5665245414306999683 ) ) ;
#4304=CIRCLE ( 'NONE', #63436, 0.9999997023190999590 ) ;
#4310=CARTESIAN_POINT ( 'NONE',  ( 4.400028935372505501, -1.270524258233924453, 0.06756676468397571078 ) ) ;
#4317=LINE ( 'NONE', #9563, #1481 ) ;
#4332=DIRECTION ( 'NONE',  ( 1.000000000000000000, 0.000000000000000000, 0.000000000000000000 ) ) ;
#4333=CARTESIAN_POINT ( 'NONE',  ( 4.659193173016666911, -0.3926218265389189721, -1.460959015002473604 ) ) ;
#4346=CARTESIAN_POINT ( 'NONE',  ( 6.513288077784000762, 0.7188269793800999841, -0.9308427218166001049 ) ) ;
#4358=CARTESIAN_POINT ( 'NONE',  ( 5.241063833726999910, -0.5918267827669999592, 1.016258213757999851 ) ) ;
#4372=LINE ( 'NONE', #19433, #56176 ) ;
#4380=EDGE_LOOP ( 'NONE', ( #66659, #68072 ) ) ;
#4420=CARTESIAN_POINT ( 'NONE',  ( 6.782661737893000087, -0.3582968336244000129, -1.367819579490999971 ) ) ;
#4446=VERTEX_POINT ( 'NONE', #43129 ) ;
#4459=CARTESIAN_POINT ( 'NONE',  ( 6.899999438051000133, 0.5526611926744998682, 1.394476821647000042 ) ) ;
#4610=CARTESIAN_POINT ( 'NONE',  ( 4.763789736435000144, -0.8239865257563000478, 0.7797128048906999398 ) ) ;
#4642=EDGE_CURVE ( 'NONE', #7462, #146, #55985, .T. ) ;
#4667=CARTESIAN_POINT ( 'NONE',  ( 5.855026506350000659, 1.500000000000000000, 0.000000000000000000 ) ) ;
#4671=PLANE ( 'NONE',  #20567 ) ;
#4686=CARTESIAN_POINT ( 'NONE',  ( 6.664531036635000127, 0.6479012572794000668, 0.9815235057283998588 ) ) ;
#4697=CARTESIAN_POINT ( 'NONE',  ( 5.593964071046000797, 1.139611800844000156, 0.2906295266426999757 ) ) ;
#4711=ORIENTED_EDGE ( 'NONE', *, *, #49497, .T. ) ;
#4723=ORIENTED_EDGE ( 'NONE', *, *, #66656, .T. ) ;
#4726=CARTESIAN_POINT ( 'NONE',  ( 4.953413393859332992, 0.4964519701263341855, 1.434320509598690840 ) ) ;
#4741=AXIS2_PLACEMENT_3D ( 'NONE', #402, #38497, #1100 ) ;
#4762=CARTESIAN_POINT ( 'NONE',  ( 7.068995775811000470, -1.403536588851999944, 0.5576917437232999930 ) ) ;
#4846=DIRECTION ( 'NONE',  ( 1.000000000000000000, 0.000000000000000000, 0.000000000000000000 ) ) ;
#4850=CARTESIAN_POINT ( 'NONE',  ( 1.700000000000000178, 0.000000000000000000, 0.000000000000000000 ) ) ;
#4877=CARTESIAN_POINT ( 'NONE',  ( 7.400000000000000355, 0.000000000000000000, 0.000000000000000000 ) ) ;
#4879=CARTESIAN_POINT ( 'NONE',  ( 5.615443173016667622, -1.500000000000000222, -0.1963495408493622085 ) ) ;
#4933=CARTESIAN_POINT ( 'NONE',  ( 5.136371739860884134, 0.9084939932534207285, 0.7817311076636899170 ) ) ;
#4960=CARTESIAN_POINT ( 'NONE',  ( 5.242725847550000040, -0.5733688592043999499, 0.9387623512300999895 ) ) ;
#4989=CARTESIAN_POINT ( 'NONE',  ( 7.167068301985500156, 0.5244239808134111280, 1.015631163775551515 ) ) ;
#5019=CARTESIAN_POINT ( 'NONE',  ( 6.052943173016667622, -1.199500263597274685, 0.9218200799623673669 ) ) ;
#5034=EDGE_CURVE ( 'NONE', #68681, #50848, #62325, .T. ) ;
#5075=CARTESIAN_POINT ( 'NONE',  ( 5.427943173017375500, 0.9218200799623694763, 1.199500263597272465 ) ) ;
#5083=CARTESIAN_POINT ( 'NONE',  ( 5.219609839683791996, -0.1963495408493605987, -1.500000000000000444 ) ) ;
#5114=CARTESIAN_POINT ( 'NONE',  ( 6.981910531964000910, 1.102261652484999965, 0.8856219692879000460 ) ) ;
#5128=CARTESIAN_POINT ( 'NONE',  ( 5.305026506349999948, 1.500000000000000000, 0.000000000000000000 ) ) ;
#5199=CARTESIAN_POINT ( 'NONE',  ( 6.829081922979999497, -1.130182777988000042, -0.07094392349790000496 ) ) ;
#5216=ORIENTED_EDGE ( 'NONE', *, *, #7479, .T. ) ;
#5245=DIRECTION ( 'NONE',  ( 0.000000000000000000, -0.9999503185633161761, -0.009967968956736161443 ) ) ;
#5248=ADVANCED_BREP_SHAPE_REPRESENTATION ( '', ( #52451, #9676 ), #67824 ) ;
#5278=CARTESIAN_POINT ( 'NONE',  ( 4.442561091537439388, -0.1847101713110425592, -1.159272428408197220 ) ) ;
#5302=CARTESIAN_POINT ( 'NONE',  ( 4.695370291990000666, 0.05305521156200000005, 1.133177390024999953 ) ) ;
#5318=FACE_OUTER_BOUND ( 'NONE', #52978, .T. ) ;
#5327=CARTESIAN_POINT ( 'NONE',  ( 4.400000000000000355, -0.7080094843779000113, -0.8552562627201000245 ) ) ;
#5331=CARTESIAN_POINT ( 'NONE',  ( 7.233484566675572047, -0.4004848424655320094, 1.070581206862469159 ) ) ;
#5342=VECTOR ( 'NONE', #49677, 1000.000000000000000 ) ;
#5386=CARTESIAN_POINT ( 'NONE',  ( 6.052891324326999722, 0.002905985354531999496, 1.468509142934999900 ) ) ;
#5431=CARTESIAN_POINT ( 'NONE',  ( 4.624349045621999998, -1.088952042328000136, -1.113569975696999892 ) ) ;
#5449=AXIS2_PLACEMENT_3D ( 'NONE', #32598, #17904, #59501 ) ;
#5465=CARTESIAN_POINT ( 'NONE',  ( 6.882286134928000010, 1.186537294537999943, -0.7690490643353999900 ) ) ;
#5491=CARTESIAN_POINT ( 'NONE',  ( 6.344609839683333696, 1.500000000000000888, -0.1963495408493590444 ) ) ;
#5515=CARTESIAN_POINT ( 'NONE',  ( 7.123756830750108904, 1.021180222699791917, -0.7836994991100844077 ) ) ;
#5546=CARTESIAN_POINT ( 'NONE',  ( -0.2999999999999999889, -1.154700538379000108, 0.000000000000000000 ) ) ;
#5570=CARTESIAN_POINT ( 'NONE',  ( 5.709193173016666734, -0.3926218265389190276, -1.460959015002473826 ) ) ;
#5581=CARTESIAN_POINT ( 'NONE',  ( 5.627943173016957346, -0.9218200799623714747, -1.199500263597270466 ) ) ;
#5648=EDGE_CURVE ( 'NONE', #39123, #11589, #544, .T. ) ;
#5651=CARTESIAN_POINT ( 'NONE',  ( 4.740443173016209322, 0.1963495408493638184, -1.499999999999999778 ) ) ;
#5665=CARTESIAN_POINT ( 'NONE',  ( 6.213089017450689866, -0.1141077043353598275, 1.127819592361385848 ) ) ;
#5667=CARTESIAN_POINT ( 'NONE',  ( 0.7000000000000000666, 0.5773502691895999739, 1.000000000000000000 ) ) ;
#5670=CARTESIAN_POINT ( 'NONE',  ( 7.034235772605498482, 0.9591814253079407049, -0.6216893316854109619 ) ) ;
#5693=CARTESIAN_POINT ( 'NONE',  ( 4.823209043203000590, 0.3714911358654000018, -1.434864438388000041 ) ) ;
#5711=CARTESIAN_POINT ( 'NONE',  ( 4.596693173016666023, -1.310679582531386389, -0.7554284705563492075 ) ) ;
#5722=CARTESIAN_POINT ( 'NONE',  ( 5.728532185269999744, -1.238562288345000040, 0.4630760545261999872 ) ) ;
#5725=ORIENTED_EDGE ( 'NONE', *, *, #32832, .F. ) ;
#5760=CARTESIAN_POINT ( 'NONE',  ( 6.284193173016666911, 1.460959015002474493, -0.3926218265389176953 ) ) ;
#5766=CARTESIAN_POINT ( 'NONE',  ( 4.521719878954000293, -1.371967559285000027, 0.7372657696301000430 ) ) ;
#5798=CARTESIAN_POINT ( 'NONE',  ( 6.670498187669999801, -0.9697342503638000100, -1.215263594530000102 ) ) ;
#5821=CARTESIAN_POINT ( 'NONE',  ( 5.953532185270000276, -1.375515609181000132, 0.5142804259680000545 ) ) ;
#5845=CARTESIAN_POINT ( 'NONE',  ( 3.400000000000000355, 1.500000000000000000, 0.000000000000000000 ) ) ;
#5862=CARTESIAN_POINT ( 'NONE',  ( 5.227606837614000135, -0.3108367803229999948, 1.065889863396000115 ) ) ;
#5877=CARTESIAN_POINT ( 'NONE',  ( 6.703785368954362944, -0.9921252471994713718, 0.7441235177248552990 ) ) ;
#5878=LINE ( 'NONE', #58681, #31660 ) ;
#5883=CARTESIAN_POINT ( 'NONE',  ( 7.360284615040999512, -1.128968895613000178, 0.4485929593892000189 ) ) ;
#5910=ORIENTED_EDGE ( 'NONE', *, *, #9605, .F. ) ;
#5911=CARTESIAN_POINT ( 'NONE',  ( 5.844609839683332808, 1.500000000000000888, -0.1963495408493590444 ) ) ;
#5918=EDGE_CURVE ( 'NONE', #39559, #49026, #27261, .T. ) ;
#5941=SURFACE_SIDE_STYLE ('',( #59776 ) ) ;
#5963=CARTESIAN_POINT ( 'NONE',  ( 5.184649729920792538, 0.2901060309370289136, 1.137486352124640776 ) ) ;
#6008=CARTESIAN_POINT ( 'NONE',  ( 5.599062476606316174, 1.099716160431485346, 0.2739963443920760966 ) ) ;
#6037=CARTESIAN_POINT ( 'NONE',  ( 4.496969878954000244, 0.5190299378403000485, -1.067582673698000084 ) ) ;
#6069=CARTESIAN_POINT ( 'NONE',  ( 5.605830324680001198, 1.139611800844000156, 0.2906295266426999757 ) ) ;
#6102=ORIENTED_EDGE ( 'NONE', *, *, #8215, .T. ) ;
#6109=CARTESIAN_POINT ( 'NONE',  ( 5.321681265427999463, -0.6446507492830000352, 1.055470389442999979 ) ) ;
#6126=EDGE_CURVE ( 'NONE', #46886, #146, #18093, .T. ) ;
#6141=CARTESIAN_POINT ( 'NONE',  ( 6.770122584706000701, 0.8499847235081999797, -1.301835277045000128 ) ) ;
#6160=CARTESIAN_POINT ( 'NONE',  ( 5.802289226419000023, 0.9320062393831999303, 1.134853260389000029 ) ) ;
#6166=CARTESIAN_POINT ( 'NONE',  ( 6.177943173016666734, -0.9218200799623716968, -1.199500263597270910 ) ) ;
#6167=ORIENTED_EDGE ( 'NONE', *, *, #63478, .F. ) ;
#6172=ORIENTED_EDGE ( 'NONE', *, *, #51709, .F. ) ;
#6226=CARTESIAN_POINT ( 'NONE',  ( 7.426573454271000685, -1.235669854462000172, 0.4909903177977000266 ) ) ;
#6237=VERTEX_POINT ( 'NONE', #15314 ) ;
#6243=VERTEX_POINT ( 'NONE', #4459 ) ;
#6267=CARTESIAN_POINT ( 'NONE',  ( 5.659193173017082579, -0.3926218265389189721, -1.460959015002473604 ) ) ;
#6351=CARTESIAN_POINT ( 'NONE',  ( 5.825282781127412157, -1.130605421812246769, 0.06802564610632597097 ) ) ;
#6366=LINE ( 'NONE', #48337, #51523 ) ;
#6379=PLANE ( 'NONE',  #28515 ) ;
#6380=CARTESIAN_POINT ( 'NONE',  ( 4.959431403105000413, 0.2984107933419999914, 1.602071312762000099 ) ) ;
#6412=CARTESIAN_POINT ( 'NONE',  ( 5.476460587185000506, 1.226089021931999978, -0.4951583500558000006 ) ) ;
#6443=CARTESIAN_POINT ( 'NONE',  ( 4.805026506350000837, 1.500000000000000000, 0.000000000000000000 ) ) ;
#6455=CARTESIAN_POINT ( 'NONE',  ( 4.682232516634000419, 1.148342943587000065, -0.8292968885249999422 ) ) ;
#6499=CARTESIAN_POINT ( 'NONE',  ( 6.998282674564999972, -1.401716800305999877, -2.564925509195000141E-10 ) ) ;
#6512=CARTESIAN_POINT ( 'NONE',  ( 6.810575618758000438, 0.8089969479913999839, 1.225571816066999942 ) ) ;
#6533=DIRECTION ( 'NONE',  ( 1.000000000000000000, 0.000000000000000000, 0.000000000000000000 ) ) ;
#6547=CARTESIAN_POINT ( 'NONE',  ( 7.143568539511687909, 1.224060264657293562, -0.3280695054382070097 ) ) ;
#6578=CARTESIAN_POINT ( 'NONE',  ( 7.260787643466000141, -0.7925871808662000584, 0.8087861320687000921 ) ) ;
#6618=DIRECTION ( 'NONE',  ( -0.7071070951631277524, 0.7071064672098279491, 3.067185053825119010E-10 ) ) ;
#6702=CARTESIAN_POINT ( 'NONE',  ( 6.762481185574685583, -0.7530625793056462403, 0.8466959786579407732 ) ) ;
#6711=ORIENTED_EDGE ( 'NONE', *, *, #979, .T. ) ;
#6760=CARTESIAN_POINT ( 'NONE',  ( 6.484746979524000032, 1.270915225504000157, -0.3650349355777000038 ) ) ;
#6824=VERTEX_POINT ( 'NONE', #56344 ) ;
#6830=CYLINDRICAL_SURFACE ( 'NONE', #1707, 1.500000000000000000 ) ;
#6856=CARTESIAN_POINT ( 'NONE',  ( 6.760161299141000057, 1.377540824270000019, 0.5088348457508999889 ) ) ;
#6861=CARTESIAN_POINT ( 'NONE',  ( -0.2999999999999999889, 0.000000000000000000, 0.000000000000000000 ) ) ;
#6886=CARTESIAN_POINT ( 'NONE',  ( 1.700000000000000178, 0.000000000000000000, 0.000000000000000000 ) ) ;
#6891=DIRECTION ( 'NONE',  ( 0.000000000000000000, -1.000000000000000000, 0.000000000000000000 ) ) ;
#6927=VERTEX_POINT ( 'NONE', #9812 ) ;
#7001=VERTEX_POINT ( 'NONE', #33907 ) ;
#7054=CARTESIAN_POINT ( 'NONE',  ( 6.746322592394366602, -0.5615255549191391360, 0.9835864943946899253 ) ) ;
#7080=CARTESIAN_POINT ( 'NONE',  ( 4.819736545624000890, -1.162446983990999883, 0.2403212362009999881 ) ) ;
#7089=CARTESIAN_POINT ( 'NONE',  ( 4.425837751058333325, 0.07782213664712105128, 1.517643997376458609 ) ) ;
#7114=CARTESIAN_POINT ( 'NONE',  ( 5.016063833727000265, -0.8125565852189000626, 1.395285458375999932 ) ) ;
#7181=FACE_OUTER_BOUND ( 'NONE', #3464, .T. ) ;
#7200=CARTESIAN_POINT ( 'NONE',  ( 7.004886577543231851, -1.395112899767755987, -0.1834843011541621716 ) ) ;
#7212=CARTESIAN_POINT ( 'NONE',  ( 6.486216479700000370, -0.9533226957039999672, 1.303269410926999994 ) ) ;
#7228=CARTESIAN_POINT ( 'NONE',  ( 6.555026506349999948, -1.500000000000000000, 0.000000000000000000 ) ) ;
#7242=CARTESIAN_POINT ( 'NONE',  ( 5.825859839684249586, 1.460959015002472494, 0.3926218265389232465 ) ) ;
#7319=CARTESIAN_POINT ( 'NONE',  ( 6.419609839683333874, 0.1963495408493571848, 1.500000000000000666 ) ) ;
#7343=CARTESIAN_POINT ( 'NONE',  ( 3.350000000000000089, 0.000000000000000000, 0.000000000000000000 ) ) ;
#7396=CARTESIAN_POINT ( 'NONE',  ( 5.389000765264640336, -0.8358857551952053599, -0.7645196268596808897 ) ) ;
#7455=CARTESIAN_POINT ( 'NONE',  ( 5.952062685092999850, 1.402153912072999997, 0.4364538398439999911 ) ) ;
#7462=VERTEX_POINT ( 'NONE', #59409 ) ;
#7479=EDGE_CURVE ( 'NONE', #53059, #24256, #28312, .T. ) ;
#7529=DIRECTION ( 'NONE',  ( 0.000000000000000000, 1.000000000000000000, 0.000000000000000000 ) ) ;
#7549=CARTESIAN_POINT ( 'NONE',  ( 5.499803308717000405, -1.431922326323000094, -0.3257311615064000243 ) ) ;
#7586=CARTESIAN_POINT ( 'NONE',  ( 6.055026506350000837, -1.500000000000000000, 0.000000000000000000 ) ) ;
#7598=CARTESIAN_POINT ( 'NONE',  ( 6.605026506349999771, -1.500000000000000000, 0.000000000000000000 ) ) ;
#7614=CARTESIAN_POINT ( 'NONE',  ( 5.805026506351000037, 1.500000000000000000, 0.000000000000000000 ) ) ;
#7617=EDGE_CURVE ( 'NONE', #62212, #58209, #49172, .T. ) ;
#7750=CARTESIAN_POINT ( 'NONE',  ( 5.356683578904362086, -1.067991396972500784, -0.3776072067835719026 ) ) ;
#7774=FACE_OUTER_BOUND ( 'NONE', #65599, .T. ) ;
#7793=ORIENTED_EDGE ( 'NONE', *, *, #26616, .F. ) ;
#7806=CARTESIAN_POINT ( 'NONE',  ( 5.772278627981999755, 0.9190761964769998960, -1.327642370976000130 ) ) ;
#7842=FACE_OUTER_BOUND ( 'NONE', #46897, .T. ) ;
#7852=DIRECTION ( 'NONE',  ( 1.000000000000000000, 0.000000000000000000, 0.000000000000000000 ) ) ;
#7883=EDGE_CURVE ( 'NONE', #67571, #37125, #69054, .T. ) ;
#7903=CARTESIAN_POINT ( 'NONE',  ( 6.529962922412000381, 0.03180299129944000325, -1.321917036380999999 ) ) ;
#7948=ORIENTED_EDGE ( 'NONE', *, *, #68351, .T. ) ;
#8009=CARTESIAN_POINT ( 'NONE',  ( 5.019676782403333704, -0.7288346947182942070, 1.349937054441816775 ) ) ;
#8020=DIRECTION ( 'NONE',  ( 0.000000000000000000, -1.000000000000000000, 0.000000000000000000 ) ) ;
#8021=CARTESIAN_POINT ( 'NONE',  ( 5.411172656737999631, 0.4773362029658999584, 1.482571116122999966 ) ) ;
#8022=ADVANCED_FACE ( 'NONE', ( #27016, #47993 ), #21753, .T. ) ;
#8120=FACE_BOUND ( 'NONE', #4380, .T. ) ;
#8134=EDGE_CURVE ( 'NONE', #40685, #54822, #28385, .T. ) ;
#8179=DIRECTION ( 'NONE',  ( 0.000000000000000000, 0.000000000000000000, 1.000000000000000000 ) ) ;
#8215=EDGE_CURVE ( 'NONE', #3750, #40516, #46711, .T. ) ;
#8236=FACE_OUTER_BOUND ( 'NONE', #50299, .T. ) ;
#8245=CARTESIAN_POINT ( 'NONE',  ( 5.471262210455999586, -0.8655273653155000080, -0.9996707749736001292 ) ) ;
#8266=CARTESIAN_POINT ( 'NONE',  ( 5.552943173016877232, -1.199500263597274685, 0.9218200799623673669 ) ) ;
#8270=B_SPLINE_CURVE_WITH_KNOTS ( 'NONE', 3,
 ( #28009, #1433, #12614, #44096 ),
 .UNSPECIFIED., .F., .F.,
 ( 4, 4 ),
 ( 0.000000000000000000, 1.000000000000000000 ),
 .UNSPECIFIED. ) ;
#8315=ORIENTED_EDGE ( 'NONE', *, *, #27574, .F. ) ;
#8325=CARTESIAN_POINT ( 'NONE',  ( 5.190443173016666023, 0.1963495408493637351, -1.499999999999999778 ) ) ;
#8379=CARTESIAN_POINT ( 'NONE',  ( -0.2999999999999999889, -1.154700538379000108, 0.000000000000000000 ) ) ;
#8411=CARTESIAN_POINT ( 'NONE',  ( 4.855026506350000659, 1.500000000000000000, 0.000000000000000000 ) ) ;
#8412=DIRECTION ( 'NONE',  ( 1.000000000000000000, 0.000000000000000000, 0.000000000000000000 ) ) ;
#8425=VECTOR ( 'NONE', #23958, 1000.000000000000000 ) ;
#8469=CARTESIAN_POINT ( 'NONE',  ( 4.367692514209000620, 1.585437927459000029, 0.3774489839997999807 ) ) ;
#8536=CARTESIAN_POINT ( 'NONE',  ( 4.400000000000000355, -0.7080094843779000113, -0.8552562627201000245 ) ) ;
#8585=CARTESIAN_POINT ( 'NONE',  ( 5.946864308364999907, -0.03293945794144000072, -1.175625617539999945 ) ) ;
#8610=CARTESIAN_POINT ( 'NONE',  ( 5.584193173016749334, -1.460959015002474937, 0.3926218265389144757 ) ) ;
#8681=ORIENTED_EDGE ( 'NONE', *, *, #55577, .T. ) ;
#8716=ADVANCED_FACE ( 'NONE', ( #37770 ), #16780, .F. ) ;
#8736=CARTESIAN_POINT ( 'NONE',  ( 7.326821631775000121, 1.159189395797000088, 0.9313610730889000378 ) ) ;
#8778=ORIENTED_EDGE ( 'NONE', *, *, #43879, .T. ) ;
#8810=CARTESIAN_POINT ( 'NONE',  ( 4.475281403099000244, -0.02432966049531000083, 1.629565400900000016 ) ) ;
#8883=CARTESIAN_POINT ( 'NONE',  ( 4.400037259600882322, -0.9678509383598562499, 0.9369558473984443969 ) ) ;
#9007=EDGE_CURVE ( 'NONE', #39123, #44844, #60398, .T. ) ;
#9093=CARTESIAN_POINT ( 'NONE',  ( 5.061409705193999464, -0.1429527940584000290, 1.396516134632999950 ) ) ;
#9098=ORIENTED_EDGE ( 'NONE', *, *, #13106, .F. ) ;
#9141=FACE_OUTER_BOUND ( 'NONE', #57242, .T. ) ;
#9186=CARTESIAN_POINT ( 'NONE',  ( 6.655923744767410888, -0.4625088890374065564, -1.452003029584873595 ) ) ;
#9212=ADVANCED_FACE ( 'NONE', ( #25631 ), #36461, .T. ) ;
#9226=B_SPLINE_CURVE_WITH_KNOTS ( 'NONE', 3,
 ( #15579, #37581, #36907, #4726, #26417, #26769, #36557, #58915, #15911, #30979 ),
 .UNSPECIFIED., .F., .F.,
 ( 4, 2, 2, 2, 4 ),
 ( 0.000000000000000000, 0.2500000000000000000, 0.5000000000000000000, 0.7500000000000000000, 1.000000000000000000 ),
 .UNSPECIFIED. ) ;
#9319=CARTESIAN_POINT ( 'NONE',  ( 7.147951193688999005, -1.276447038156000025, 0.5071930294755999657 ) ) ;
#9442=CARTESIAN_POINT ( 'NONE',  ( 7.399999875133000060, -0.9999998751120001694, -1.219899823892999791E-10 ) ) ;
#9510=CARTESIAN_POINT ( 'NONE',  ( 4.353273069765999814, -1.059004588577999950, -0.4067126231303999639 ) ) ;
#9526=PLANE ( 'NONE',  #13124 ) ;
#9529=CARTESIAN_POINT ( 'NONE',  ( 6.842747251585779900, 1.356930585311906690, 0.6940459256229121188 ) ) ;
#9540=CARTESIAN_POINT ( 'NONE',  ( 4.982109839683335650, -0.9218200799623778030, 1.199500263597266914 ) ) ;
#9563=CARTESIAN_POINT ( 'NONE',  ( 5.305026506349999948, 1.500000000000000000, 0.000000000000000000 ) ) ;
#9605=EDGE_CURVE ( 'NONE', #67571, #27153, #66630, .T. ) ;
#9634=CARTESIAN_POINT ( 'NONE',  ( 5.308543490071000015, 1.556797599500999940, -0.04728230666302999513 ) ) ;
#9665=CARTESIAN_POINT ( 'NONE',  ( 6.695576494045999638, -0.8862304417126000144, 0.8626632806168000878 ) ) ;
#9676=AXIS2_PLACEMENT_3D ( 'NONE', #40345, #19020, #18341 ) ;
#9736=EDGE_CURVE ( 'NONE', #65585, #63838, #26155, .T. ) ;
#9788=STYLED_ITEM ( 'NONE', ( #21674 ), #5248 ) ;
#9812=CARTESIAN_POINT ( 'NONE',  ( 4.805026506350000837, 1.500000000000000000, 0.000000000000000000 ) ) ;
#9849=CIRCLE ( 'NONE', #33267, 0.5000000000000000000 ) ;
#9862=CARTESIAN_POINT ( 'NONE',  ( 5.150632654315000281, 1.274863079208999883, -0.03871952724233999887 ) ) ;
#9878=ADVANCED_FACE ( 'NONE', ( #22277 ), #28222, .T. ) ;
#9931=VERTEX_POINT ( 'NONE', #48857 ) ;
#9984=CARTESIAN_POINT ( 'NONE',  ( 4.966446267845999962, -0.5822046538191000264, 1.444608038638999892 ) ) ;
#9985=CARTESIAN_POINT ( 'NONE',  ( 5.157109839683540642, -1.199500263597270022, -0.9218200799623730290 ) ) ;
#10015=CARTESIAN_POINT ( 'NONE',  ( 7.136881816240999932, -1.205895524350000025, 0.6847492370762000569 ) ) ;
#10044=ORIENTED_EDGE ( 'NONE', *, *, #21080, .T. ) ;
#10059=VECTOR ( 'NONE', #31397, 1000.000000000000000 ) ;
#10062=LINE ( 'NONE', #14628, #10059 ) ;
#10087=EDGE_CURVE ( 'NONE', #58209, #46886, #24551, .T. ) ;
#10134=CARTESIAN_POINT ( 'NONE',  ( 5.834193173016667622, 1.460959015002474048, -0.3926218265389178064 ) ) ;
#10207=CARTESIAN_POINT ( 'NONE',  ( 5.219052098759999758, 0.8613139015395000486, 0.9406969777927000065 ) ) ;
#10209=CARTESIAN_POINT ( 'NONE',  ( 4.400000000000000355, 1.266759534686000110, 0.8033182938792000627 ) ) ;
#10339=CARTESIAN_POINT ( 'NONE',  ( 4.485427710978749261, -0.1089645256540823087, 1.530309145191555364 ) ) ;
#10361=CARTESIAN_POINT ( 'NONE',  ( 7.139821367719000555, 0.8827681146003000245, 0.7092679259177999684 ) ) ;
#10386=CARTESIAN_POINT ( 'NONE',  ( 6.282109839683333696, 0.9218200799623742503, -1.199500263597268912 ) ) ;
#10414=ORIENTED_EDGE ( 'NONE', *, *, #47128, .F. ) ;
#10416=ORIENTED_EDGE ( 'NONE', *, *, #47128, .T. ) ;
#10438=CARTESIAN_POINT ( 'NONE',  ( 6.055026506350000837, -1.500000000000000000, 0.000000000000000000 ) ) ;
#10443=CARTESIAN_POINT ( 'NONE',  ( 6.961532175979001202, -1.035056448321000078, 1.007531618533000106 ) ) ;
#10470=CARTESIAN_POINT ( 'NONE',  ( 5.802943173016667622, 1.199500263597271799, -0.9218200799623701425 ) ) ;
#10546=CARTESIAN_POINT ( 'NONE',  ( 4.329599320976000421, -0.7696520519970999619, 1.017058582320000015 ) ) ;
#10549=CARTESIAN_POINT ( 'NONE',  ( 4.555026506349999948, -1.500000000000000000, 0.000000000000000000 ) ) ;
#10578=B_SPLINE_CURVE_WITH_KNOTS ( 'NONE', 3,
 ( #27051, #127, #31605, #43122, #820, #10613, #58854, #15524, #37878, #48718, #26362, #42095, #68999, #31953, #48024, #11299, #10964, #68647 ),
 .UNSPECIFIED., .F., .F.,
 ( 4, 2, 2, 2, 2, 2, 2, 2, 4 ),
 ( 0.000000000000000000, 0.1249999999999999445, 0.2499999999999998890, 0.3749999999999998890, 0.4999999999999997780, 0.6249999999999997780, 0.7499999999999998890, 0.8749999999999998890, 1.000000000000000000 ),
 .UNSPECIFIED. ) ;
#10587=ORIENTED_EDGE ( 'NONE', *, *, #40265, .F. ) ;
#10613=CARTESIAN_POINT ( 'NONE',  ( 4.399744774746779719, 0.1610061330520185519, -1.221142052500258313 ) ) ;
#10614=CARTESIAN_POINT ( 'NONE',  ( 4.784193173016666911, 1.460959015002474493, -0.3926218265389176953 ) ) ;
#10628=CARTESIAN_POINT ( 'NONE',  ( 6.153719963560999595, -1.400415568386000009, 0.4419997549869000286 ) ) ;
#10671=CARTESIAN_POINT ( 'NONE',  ( 4.396284230805000526, 0.7308517094458000241, 1.339263914767000019 ) ) ;
#10694=CARTESIAN_POINT ( 'NONE',  ( 6.355026506350000659, 1.500000000000000000, 0.000000000000000000 ) ) ;
#10701=CARTESIAN_POINT ( 'NONE',  ( 7.094074082186000219, 0.5841380621085999758, 1.131277061175999910 ) ) ;
#10878=DIRECTION ( 'NONE',  ( 1.000000000000000000, 0.000000000000000000, 0.000000000000000000 ) ) ;
#10884=MECHANICAL_DESIGN_GEOMETRIC_PRESENTATION_REPRESENTATION('',(#9788),#31010);
#10892=CARTESIAN_POINT ( 'NONE',  ( 4.524321680877999796, 0.9196732308882999973, -0.6641588674314000684 ) ) ;
#10912=ORIENTED_EDGE ( 'NONE', *, *, #4642, .T. ) ;
#10924=CARTESIAN_POINT ( 'NONE',  ( 7.263286839971717868, -0.7590492731972352525, 0.8424490475276925627 ) ) ;
#10946=CARTESIAN_POINT ( 'NONE',  ( 5.153205201823999992, -0.3383038778767000210, 1.221805324548000060 ) ) ;
#10964=CARTESIAN_POINT ( 'NONE',  ( 4.399614530587001582, 1.347590462918873522, 0.6451537652597036931 ) ) ;
#10965=CARTESIAN_POINT ( 'NONE',  ( 4.763359839683333874, 1.310679582531388387, -0.7554284705563470981 ) ) ;
#10977=CARTESIAN_POINT ( 'NONE',  ( 6.736818577609000158, -1.197190821580000009, 0.3103650564550000102 ) ) ;
#10993=VECTOR ( 'NONE', #37537, 1000.000000000000000 ) ;
#11015=CARTESIAN_POINT ( 'NONE',  ( 6.221693173016666023, 0.7554284705563509839, -1.310679582531386167 ) ) ;
#11020=CARTESIAN_POINT ( 'NONE',  ( 4.921700572190999878, -1.028864471296000005, 0.9735824284629999159 ) ) ;
#11031=CARTESIAN_POINT ( 'NONE',  ( 4.519598795370249888, -0.7275289865389679145, 1.350711265020586138 ) ) ;
#11074=CARTESIAN_POINT ( 'NONE',  ( 6.054360824503000948, -0.9021507525358000157, -1.158728426834999992 ) ) ;
#11137=CARTESIAN_POINT ( 'NONE',  ( 7.094746981741000269, 1.094478228765999983, 0.2906167377007999875 ) ) ;
#11190=( NAMED_UNIT ( * ) PLANE_ANGLE_UNIT ( ) SI_UNIT ( $, .RADIAN. ) );
#11200=EDGE_CURVE ( 'NONE', #3150, #40878, #63896, .T. ) ;
#11206=AXIS2_PLACEMENT_3D ( 'NONE', #59192, #54288, #32634 ) ;
#11233=CARTESIAN_POINT ( 'NONE',  ( 4.159417977171999681, 0.5323169164456000857, 0.9754548401560999560 ) ) ;
#11284=CARTESIAN_POINT ( 'NONE',  ( 5.009753349970999636, 1.333795246837999882, 0.04609146662756000157 ) ) ;
#11295=CARTESIAN_POINT ( 'NONE',  ( 5.907109839683334584, 1.199500263597268246, 0.9218200799623752495 ) ) ;
#11299=CARTESIAN_POINT ( 'NONE',  ( 4.399622670846948580, 1.399596316936216223, 0.4756535215918837878 ) ) ;
#11313=CARTESIAN_POINT ( 'NONE',  ( 5.252930087360999423, -0.5918267827669999592, 1.016258213757999851 ) ) ;
#11351=CARTESIAN_POINT ( 'NONE',  ( 6.055026506350000837, -1.500000000000000000, 0.000000000000000000 ) ) ;
#11356=CARTESIAN_POINT ( 'NONE',  ( 4.340135294409000366, 0.2980381316198000285, 1.384766116913999978 ) ) ;
#11408=CARTESIAN_POINT ( 'NONE',  ( 6.587045118934000243, -1.528745275297999973, -0.5198780721924000092 ) ) ;
#11415=CARTESIAN_POINT ( 'NONE',  ( 6.334193173016667622, 1.460959015002474048, -0.3926218265389178064 ) ) ;
#11443=CARTESIAN_POINT ( 'NONE',  ( 5.888359839683998231, 0.7554284705563452107, 1.310679582531388609 ) ) ;
#11472=CARTESIAN_POINT ( 'NONE',  ( 7.360157189579999759, -0.4795858584850000161, 1.282035055333999862 ) ) ;
#11589=VERTEX_POINT ( 'NONE', #63121 ) ;
#11595=CARTESIAN_POINT ( 'NONE',  ( 5.631379662966172539, 0.9049817462873084306, 0.6808242691568766602 ) ) ;
#11625=CARTESIAN_POINT ( 'NONE',  ( 4.633192238856000067, -0.01992358281169000211, 1.334452703055000189 ) ) ;
#11657=CARTESIAN_POINT ( 'NONE',  ( 5.274803308717000760, -1.289352866216999960, -0.2932997125499000046 ) ) ;
#11658=CARTESIAN_POINT ( 'NONE',  ( 6.553816671982000130, -1.199981415667000118, 0.9000247785775999931 ) ) ;
#11692=CARTESIAN_POINT ( 'NONE',  ( 6.305026506349999948, 1.500000000000000000, 0.000000000000000000 ) ) ;
#11694=CARTESIAN_POINT ( 'NONE',  ( 6.075859839683334762, -1.460959015002473826, -0.3926218265389207485 ) ) ;
#11699=CARTESIAN_POINT ( 'NONE',  ( 4.898026823400999596, 0.7146345574896999508, 1.383890202823000237 ) ) ;
#11753=CARTESIAN_POINT ( 'NONE',  ( 6.990359675868999645, -1.019889730527999916, 1.251756626546000062 ) ) ;
#11754=B_SPLINE_CURVE_WITH_KNOTS ( 'NONE', 3,
 ( #16319, #5491, #11415, #57946, #42554, #10386, #32757, #47811, #52693, #68763, #42898, #37648, #6166, #27508, #48834, #36970, #942, #22255 ),
 .UNSPECIFIED., .F., .F.,
 ( 4, 2, 2, 2, 2, 2, 2, 2, 4 ),
 ( 0.000000000000000000, 0.1250000000000000000, 0.2500000000000000000, 0.3750000000000000000, 0.5000000000000000000, 0.6250000000000000000, 0.7500000000000000000, 0.8750000000000000000, 1.000000000000000000 ),
 .UNSPECIFIED. ) ;
#11819=CARTESIAN_POINT ( 'NONE',  ( 7.293995775811000115, -1.022267936763999963, 0.4061956009805000600 ) ) ;
#11878=SURFACE_STYLE_USAGE ( .BOTH. , #5941 ) ;
#11925=CARTESIAN_POINT ( 'NONE',  ( 4.182224458653999832, 0.2386897511459999954, 1.109017420168999957 ) ) ;
#11965=ORIENTED_EDGE ( 'NONE', *, *, #42947, .F. ) ;
#11978=CARTESIAN_POINT ( 'NONE',  ( 4.927325434513999625, -0.4869043722212999525, -1.082571524400999907 ) ) ;
#12012=CARTESIAN_POINT ( 'NONE',  ( 6.720013804402999114, -1.131649478240000173, 0.5631818380099999910 ) ) ;
#12038=AXIS2_PLACEMENT_3D ( 'NONE', #48896, #58343, #63585 ) ;
#12056=CARTESIAN_POINT ( 'NONE',  ( 4.590139323399000659, -1.453974671782999994, -0.5584015962769001140 ) ) ;
#12099=CARTESIAN_POINT ( 'NONE',  ( 4.400000000000000355, 0.5526513453421999511, 1.394480724316999876 ) ) ;
#12113=CARTESIAN_POINT ( 'NONE',  ( 6.234144881615000244, 0.9190761964769998960, -1.327642370976000130 ) ) ;
#12132=CARTESIAN_POINT ( 'NONE',  ( 5.227606837614000135, -0.3108367803229999948, 1.065889863396000115 ) ) ;
#12218=EDGE_LOOP ( 'NONE', ( #21708, #38159, #51344, #60225, #30055, #36340 ) ) ;
#12236=EDGE_CURVE ( 'NONE', #14587, #13866, #51945, .T. ) ;
#12284=CARTESIAN_POINT ( 'NONE',  ( 6.899999438051000133, 1.266765207443000030, 0.8033093483900000109 ) ) ;
#12295=LINE ( 'NONE', #23121, #26564 ) ;
#12304=CARTESIAN_POINT ( 'NONE',  ( 5.922234340208202497, -0.4543021360680231102, -1.037812024122457544 ) ) ;
#12312=ADVANCED_FACE ( 'NONE', ( #28069, #64069 ), #6379, .F. ) ;
#12333=CARTESIAN_POINT ( 'NONE',  ( 5.088708767848000747, 1.186311595762999938, 0.04099492891103999337 ) ) ;
#12339=( NAMED_UNIT ( * ) PLANE_ANGLE_UNIT ( ) SI_UNIT ( $, .RADIAN. ) );
#12349=VECTOR ( 'NONE', #53513, 1000.000000000000000 ) ;
#12424=ORIENTED_EDGE ( 'NONE', *, *, #63602, .T. ) ;
#12431=CARTESIAN_POINT ( 'NONE',  ( 5.452606837613999780, -0.4199405305951999789, 1.440017343911000003 ) ) ;
#12457=CARTESIAN_POINT ( 'NONE',  ( 5.931658963912999738, 0.08722338096739000457, 1.612367018429999854 ) ) ;
#12503=DIRECTION ( 'NONE',  ( 1.000000000000000000, 0.000000000000000000, 0.000000000000000000 ) ) ;
#12535=ADVANCED_FACE ( 'NONE', ( #30033 ), #2408, .T. ) ;
#12591=B_SPLINE_CURVE_WITH_KNOTS ( 'NONE', 3,
 ( #53781, #5877, #27216, #43177 ),
 .UNSPECIFIED., .F., .F.,
 ( 4, 4 ),
 ( 0.000000000000000000, 1.000000000000000000 ),
 .UNSPECIFIED. ) ;
#12614=CARTESIAN_POINT ( 'NONE',  ( 6.841180590298025166, -0.9745722302259033354, 0.7309630519589359610 ) ) ;
#12650=CARTESIAN_POINT ( 'NONE',  ( 6.503943694692421396, 0.6532722510427437790, -0.9258527769090765247 ) ) ;
#12671=ORIENTED_EDGE ( 'NONE', *, *, #37497, .F. ) ;
#12685=SURFACE_SIDE_STYLE ('',( #54990 ) ) ;
#12711=CARTESIAN_POINT ( 'NONE',  ( 5.419378390662999756, 1.024801514603000063, 1.247845015360000032 ) ) ;
#12728=CARTESIAN_POINT ( 'NONE',  ( 0.7000000000000000666, 0.000000000000000000, 0.000000000000000000 ) ) ;
#12740=PLANE ( 'NONE',  #58252 ) ;
#12800=DIRECTION ( 'NONE',  ( 1.000000000000000000, 0.000000000000000000, 0.000000000000000000 ) ) ;
#12808=CARTESIAN_POINT ( 'NONE',  ( 5.824162447775000473, -0.7240778834237999728, 1.106429931180000104 ) ) ;
#12829=ORIENTED_EDGE ( 'NONE', *, *, #48885, .F. ) ;
#12912=CARTESIAN_POINT ( 'NONE',  ( 5.070886616771334232, -1.393043258182025568, 0.6426200619446649220 ) ) ;
#12961=CARTESIAN_POINT ( 'NONE',  ( 5.440308476675333793, -0.1973919536007288644, 1.504917372998084923 ) ) ;
#13030=DIRECTION ( 'NONE',  ( 0.000000000000000000, 1.000000000000000000, 0.000000000000000000 ) ) ;
#13062=CARTESIAN_POINT ( 'NONE',  ( 5.973935906450000388, 0.003195320017092000316, 1.614721372341000105 ) ) ;
#13106=EDGE_CURVE ( 'NONE', #44723, #62212, #48426, .T. ) ;
#13124=AXIS2_PLACEMENT_3D ( 'NONE', #46260, #21394, #16834 ) ;
#13151=DIRECTION ( 'NONE',  ( 1.000000000000000000, 0.000000000000000000, 0.000000000000000000 ) ) ;
#13162=CARTESIAN_POINT ( 'NONE',  ( 6.580377242028999873, 0.8081923938199999657, -1.046566182397999922 ) ) ;
#13165=CYLINDRICAL_SURFACE ( 'NONE', #37697, 0.5999999999999999778 ) ;
#13221=FACE_OUTER_BOUND ( 'NONE', #44299, .T. ) ;
#13230=ORIENTED_EDGE ( 'NONE', *, *, #3397, .T. ) ;
#13243=ORIENTED_EDGE ( 'NONE', *, *, #54837, .T. ) ;
#13255=EDGE_LOOP ( 'NONE', ( #58476, #52391, #20925, #29133 ) ) ;
#13259=CARTESIAN_POINT ( 'NONE',  ( 7.399999923048000028, 0.9999997023190999590, 0.000000000000000000 ) ) ;
#13302=DIRECTION ( 'NONE',  ( 0.000000000000000000, -1.000000000000000000, 0.000000000000000000 ) ) ;
#13303=ADVANCED_FACE ( 'NONE', ( #29682 ), #62489, .F. ) ;
#13334=EDGE_LOOP ( 'NONE', ( #28713, #7793, #32259, #39296 ) ) ;
#13342=CARTESIAN_POINT ( 'NONE',  ( 4.615443173015708389, -1.500000000000000222, -0.1963495408493622085 ) ) ;
#13405=UNCERTAINTY_MEASURE_WITH_UNIT (LENGTH_MEASURE( 1.000000000000000082E-05 ), #59088, 'distance_accuracy_value', 'NONE');
#13428=CARTESIAN_POINT ( 'NONE',  ( 6.785263095641375308, 1.476230154961222452, -0.3823247283369876626 ) ) ;
#13473=CARTESIAN_POINT ( 'NONE',  ( 1.700000000000000178, 0.000000000000000000, 0.000000000000000000 ) ) ;
#13505=CARTESIAN_POINT ( 'NONE',  ( 6.350178865300000197, -1.113463867511000238, -0.3786539577593999728 ) ) ;
#13508=DIRECTION ( 'NONE',  ( -1.000000000000000000, 0.000000000000000000, 0.000000000000000000 ) ) ;
#13521=DIRECTION ( 'NONE',  ( 1.000000000000000000, 0.000000000000000000, 0.000000000000000000 ) ) ;
#13579=CARTESIAN_POINT ( 'NONE',  ( 5.127943173016667799, -0.9218200799623714747, -1.199500263597270466 ) ) ;
#13598=ORIENTED_EDGE ( 'NONE', *, *, #63478, .T. ) ;
#13615=CARTESIAN_POINT ( 'NONE',  ( 6.315443173016669576, 1.499999999999999778, 0.1963495408493654004 ) ) ;
#13619=CARTESIAN_POINT ( 'NONE',  ( 5.103285156735999806, -1.342354185336999794, -0.7898986551783000465 ) ) ;
#13662=CYLINDRICAL_SURFACE ( 'NONE', #912, 1.500000000000000000 ) ;
#13692=CARTESIAN_POINT ( 'NONE',  ( 5.243573426643169277, -0.5273870646426602748, 1.002916043689504377 ) ) ;
#13787=LINE ( 'NONE', #19716, #17341 ) ;
#13813=LINE ( 'NONE', #46998, #16127 ) ;
#13815=CARTESIAN_POINT ( 'NONE',  ( 4.565443173016666911, -1.500000000000000222, -0.1963495408493622363 ) ) ;
#13839=CARTESIAN_POINT ( 'NONE',  ( 5.924991087009000346, -1.272350122907000003, -0.3600015818555999947 ) ) ;
#13866=VERTEX_POINT ( 'NONE', #20715 ) ;
#13889=ADVANCED_FACE ( 'NONE', ( #68592, #3590 ), #9526, .F. ) ;
#13991=CARTESIAN_POINT ( 'NONE',  ( 5.305026506349999948, 1.500000000000000000, 0.000000000000000000 ) ) ;
#14086=CARTESIAN_POINT ( 'NONE',  ( 7.044509995414057535, -0.8324003622799491797, -1.084551266798225333 ) ) ;
#14107=CARTESIAN_POINT ( 'NONE',  ( 6.699036861725389258, 0.3526192069364459392, -1.483084712358169854 ) ) ;
#14119=CARTESIAN_POINT ( 'NONE',  ( 5.055026506350000837, -1.500000000000000000, 0.000000000000000000 ) ) ;
#14173=ORIENTED_EDGE ( 'NONE', *, *, #67260, .T. ) ;
#14180=CARTESIAN_POINT ( 'NONE',  ( 6.177062685093000383, 1.262548346495000029, 0.3929982786279000440 ) ) ;
#14195=EDGE_CURVE ( 'NONE', #7001, #65623, #62923, .T. ) ;
#14250=CARTESIAN_POINT ( 'NONE',  ( 6.943877770042311326, -0.7023778695283228179, 1.314805733899347739 ) ) ;
#14295=AXIS2_PLACEMENT_3D ( 'NONE', #66441, #66095, #18213 ) ;
#14305=ORIENTED_EDGE ( 'NONE', *, *, #5648, .F. ) ;
#14327=EDGE_CURVE ( 'NONE', #27153, #42702, #33464, .T. ) ;
#14337=CARTESIAN_POINT ( 'NONE',  ( 3.400000000000000355, -1.000000000000000000, 0.000000000000000000 ) ) ;
#14352=CARTESIAN_POINT ( 'NONE',  ( 5.851234045860000066, 0.8358542970315000487, -1.207425004536999857 ) ) ;
#14355=AXIS2_PLACEMENT_3D ( 'NONE', #36379, #31483, #63277 ) ;
#14407=DIRECTION ( 'NONE',  ( -0.7071069136393470789, 0.000000000000000000, -0.7071066487337230866 ) ) ;
#14479=CARTESIAN_POINT ( 'NONE',  ( 4.400035872229480560, -1.058819220088977886, 0.8053076396761240652 ) ) ;
#14514=CARTESIAN_POINT ( 'NONE',  ( 6.059559201232000092, 1.111956540095999868, -0.3830577677631999967 ) ) ;
#14525=LINE ( 'NONE', #36880, #16533 ) ;
#14576=CARTESIAN_POINT ( 'NONE',  ( -0.2999999999999999889, 1.154700538379000108, 0.000000000000000000 ) ) ;
#14587=VERTEX_POINT ( 'NONE', #22525 ) ;
#14609=AXIS2_PLACEMENT_3D ( 'NONE', #17879, #33268, #28024 ) ;
#14628=CARTESIAN_POINT ( 'NONE',  ( 1.700000000000000178, 1.500000000000000000, 0.000000000000000000 ) ) ;
#14692=CARTESIAN_POINT ( 'NONE',  ( 5.246262210455999941, -0.9612325616298000863, -1.110208802542000051 ) ) ;
#14697=ORIENTED_EDGE ( 'NONE', *, *, #40108, .T. ) ;
#14739=ORIENTED_EDGE ( 'NONE', *, *, #31098, .T. ) ;
#14773=CARTESIAN_POINT ( 'NONE',  ( 4.455902236433000319, 0.09694544799576999827, -1.130268743893000138 ) ) ;
#14837=CARTESIAN_POINT ( 'NONE',  ( 3.400000000000000355, 0.000000000000000000, 0.000000000000000000 ) ) ;
#14922=CARTESIAN_POINT ( 'NONE',  ( 7.206237632408999616, 0.06715535307188000291, 1.130410956850999904 ) ) ;
#14931=EDGE_CURVE ( 'NONE', #56519, #39559, #52176, .T. ) ;
#14982=DIRECTION ( 'NONE',  ( 0.000000000000000000, 0.5000000000000169864, -0.8660254037844288266 ) ) ;
#15008=FACE_OUTER_BOUND ( 'NONE', #12218, .T. ) ;
#15076=EDGE_LOOP ( 'NONE', ( #28274, #57582 ) ) ;
#15084=B_SPLINE_CURVE_WITH_KNOTS ( 'NONE', 3,
 ( #43815, #54286, #7089, #59880, #16541, #49742, #38209, #1851, #23169, #33325 ),
 .UNSPECIFIED., .F., .F.,
 ( 4, 2, 2, 2, 4 ),
 ( 0.000000000000000000, 0.2500000000000001110, 0.5000000000000001110, 0.7500000000000001110, 1.000000000000000000 ),
 .UNSPECIFIED. ) ;
#15113=CARTESIAN_POINT ( 'NONE',  ( 4.569067376532999880, 0.6287086875568000943, -1.109729982504999990 ) ) ;
#15176=CARTESIAN_POINT ( 'NONE',  ( 4.638359839683334762, -0.7554284705563483193, -1.310679582531387721 ) ) ;
#15191=AXIS2_PLACEMENT_3D ( 'NONE', #66992, #63807, #15237 ) ;
#15202=CARTESIAN_POINT ( 'NONE',  ( 5.694792710280000669, 0.06352927768877000836, 1.174369886990999978 ) ) ;
#15237=DIRECTION ( 'NONE',  ( 0.000000000000000000, 1.000000000000000000, 0.000000000000000000 ) ) ;
#15244=B_SPLINE_CURVE_WITH_KNOTS ( 'NONE', 3,
 ( #6443, #18330, #39654, #27791, #34424, #1212, #22523, #54692, #45928, #29529, #30885, #24255, #9540, #57099, #24943, #30205, #35443, #14119 ),
 .UNSPECIFIED., .F., .F.,
 ( 4, 2, 2, 2, 2, 2, 2, 2, 4 ),
 ( 0.000000000000000000, 0.1249999999999999722, 0.2499999999999999445, 0.3749999999999998890, 0.4999999999999998890, 0.6249999999999998890, 0.7499999999999997780, 0.8749999999999998890, 1.000000000000000000 ),
 .UNSPECIFIED. ) ;
#15259=PLANE ( 'NONE',  #21485 ) ;
#15268=CARTESIAN_POINT ( 'NONE',  ( 6.706645871493999600, -1.006228542663000214, 0.7393869427924999460 ) ) ;
#15314=CARTESIAN_POINT ( 'NONE',  ( -0.2999999999999999889, 1.154700538379000108, 0.000000000000000000 ) ) ;
#15460=CARTESIAN_POINT ( 'NONE',  ( 4.671696543201000473, 1.240591757068000067, 0.2961542510987000276 ) ) ;
#15484=ORIENTED_EDGE ( 'NONE', *, *, #4642, .F. ) ;
#15519=CARTESIAN_POINT ( 'NONE',  ( 5.805026506351000037, 1.500000000000000000, 0.000000000000000000 ) ) ;
#15520=CARTESIAN_POINT ( 'NONE',  ( 6.094609839683333696, -1.500000000000000888, 0.1963495408493559080 ) ) ;
#15524=CARTESIAN_POINT ( 'NONE',  ( 4.399720353966697139, 0.5971468265269567199, -1.134349138418559999 ) ) ;
#15525=CARTESIAN_POINT ( 'NONE',  ( 4.700859839683333874, 0.3926218265389221362, -1.460959015002473160 ) ) ;
#15579=CARTESIAN_POINT ( 'NONE',  ( 5.002606837613999602, -0.4199405305951999789, 1.440017343911000003 ) ) ;
#15584=LINE ( 'NONE', #46716, #57611 ) ;
#15613=CARTESIAN_POINT ( 'NONE',  ( 7.173029500063999642, 0.5195473280092000046, 1.006186743336999978 ) ) ;
#15692=ADVANCED_FACE ( 'NONE', ( #28981 ), #22326, .T. ) ;
#15697=CARTESIAN_POINT ( 'NONE',  ( 6.995122584706000346, 0.6190876222846001253, -0.9481936368762999834 ) ) ;
#15797=CARTESIAN_POINT ( 'NONE',  ( 4.363809043199000648, -1.123505578223999990, 0.6037476609470000533 ) ) ;
#15815=ORIENTED_EDGE ( 'NONE', *, *, #14327, .T. ) ;
#15873=CARTESIAN_POINT ( 'NONE',  ( 6.535161299140999525, 1.240385862733000000, 0.4581726639353000397 ) ) ;
#15911=CARTESIAN_POINT ( 'NONE',  ( 4.867324867288667534, 1.499999999999999778, 0.2318186422567637128 ) ) ;
#15950=CARTESIAN_POINT ( 'NONE',  ( 7.127282214532000282, 0.07550418544918999220, 1.270944974832999952 ) ) ;
#16011=CARTESIAN_POINT ( 'NONE',  ( -0.2999999999999999889, -0.5773502691895999739, 1.000000000000000000 ) ) ;
#16033=CARTESIAN_POINT ( 'NONE',  ( 7.227579511121000166, -0.3967607077929999893, 1.060625802389000061 ) ) ;
#16093=SHAPE_REPRESENTATION_RELATIONSHIP ( 'NONE' , 'NONE' ,  #26842, #5248 ) ;
#16127=VECTOR ( 'NONE', #62041, 1000.000000000000000 ) ;
#16139=CARTESIAN_POINT ( 'NONE',  ( 5.253261820982999986, 0.3908910841886000243, 1.214078939262000167 ) ) ;
#16189=CARTESIAN_POINT ( 'NONE',  ( 5.232160619701999416, -0.3008961189268999914, 1.086704895458000086 ) ) ;
#16217=CARTESIAN_POINT ( 'NONE',  ( 5.930189463737000288, 0.7526323975856999970, -1.087207638099000118 ) ) ;
#16246=LINE ( 'NONE', #58904, #23061 ) ;
#16255=CARTESIAN_POINT ( 'NONE',  ( 6.190443173016666023, 0.1963495408493637351, -1.499999999999999778 ) ) ;
#16260=CARTESIAN_POINT ( 'NONE',  ( 4.761187934510999753, 1.262677799937000023, -0.9118658990719999968 ) ) ;
#16293=CARTESIAN_POINT ( 'NONE',  ( 6.649829208513000189, -1.325979800714000012, 0.4909860521821999835 ) ) ;
#16313=CARTESIAN_POINT ( 'NONE',  ( 6.104775144120000441, -0.04112960214766999550, -1.467935932961000001 ) ) ;
#16319=CARTESIAN_POINT ( 'NONE',  ( 6.355026506350000659, 1.500000000000000000, 0.000000000000000000 ) ) ;
#16378=CARTESIAN_POINT ( 'NONE',  ( 6.862162629864999808, -1.172778741670000180, 0.4342585038969999922 ) ) ;
#16420=CARTESIAN_POINT ( 'NONE',  ( 5.700859839683917407, 0.3926218265389221362, -1.460959015002473160 ) ) ;
#16499=ORIENTED_EDGE ( 'NONE', *, *, #47837, .F. ) ;
#16504=CARTESIAN_POINT ( 'NONE',  ( 6.649371033313499879, 0.7294112533789433028, 0.8667001409038291859 ) ) ;
#16509=CARTESIAN_POINT ( 'NONE',  ( 6.834986978535497748, -1.140791068544842579, -0.07160982795898844511 ) ) ;
#16512=ORIENTED_EDGE ( 'NONE', *, *, #25108, .F. ) ;
#16514=DIRECTION ( 'NONE',  ( -1.000000000000000000, 0.000000000000000000, 0.000000000000000000 ) ) ;
#16517=EDGE_LOOP ( 'NONE', ( #66378, #65360, #42130 ) ) ;
#16532=DIRECTION ( 'NONE',  ( 0.000000000000000000, 1.000000000000000000, 0.000000000000000000 ) ) ;
#16533=VECTOR ( 'NONE', #58196, 1000.000000000000114 ) ;
#16534=CARTESIAN_POINT ( 'NONE',  ( 4.984592376538000025, 1.123536932646000075, 0.9667689356016999636 ) ) ;
#16541=CARTESIAN_POINT ( 'NONE',  ( 4.464594377645832779, -0.6414890624138858133, 1.377603488137450594 ) ) ;
#16544=DIRECTION ( 'NONE',  ( -1.000000000000000000, 0.000000000000000000, 0.000000000000000000 ) ) ;
#16563=CARTESIAN_POINT ( 'NONE',  ( 6.131846742205000034, 0.002616650692276999927, 1.322296913527999829 ) ) ;
#16606=CARTESIAN_POINT ( 'NONE',  ( 4.853281127746000401, 0.06624698400605999460, 1.414933278434000075 ) ) ;
#16656=CARTESIAN_POINT ( 'NONE',  ( 5.679587365828999701, -0.1291622704458000037, -1.609550399409999999 ) ) ;
#16780=CYLINDRICAL_SURFACE ( 'NONE', #21071, 0.5999999999999999778 ) ;
#16834=DIRECTION ( 'NONE',  ( 0.000000000000000000, 1.000000000000000000, 0.000000000000000000 ) ) ;
#16845=CARTESIAN_POINT ( 'NONE',  ( 6.374674949252075784, -0.9558318679937189977, -0.6073786151858517890 ) ) ;
#16875=CARTESIAN_POINT ( 'NONE',  ( 4.285264598750999632, -0.3285995775302999466, -1.445177149630999969 ) ) ;
#16885=CARTESIAN_POINT ( 'NONE',  ( 5.927943173016666734, 0.9218200799623694763, 1.199500263597272465 ) ) ;
#16897=CARTESIAN_POINT ( 'NONE',  ( -0.2999999999999999889, -0.5773502691895999739, -1.000000000000000000 ) ) ;
#16900=CARTESIAN_POINT ( 'NONE',  ( 5.202515767743999930, 0.1165019947749000029, 1.093825345293000018 ) ) ;
#16941=CARTESIAN_POINT ( 'NONE',  ( 4.692768490066000275, 0.1331025639088000145, -1.551817757593000113 ) ) ;
#16965=B_SPLINE_CURVE_WITH_KNOTS ( 'NONE', 3,
 ( #64383, #6702, #7054, #27348, #54953, #28043, #16504, #49351, #1813, #48670, #23133, #64729, #12650, #21744, #38167, #775, #22781, #16845, #65429, #43076, #48324, #38878, #37831, #1122, #5665, #428, #27699, #22435, #44131, #44484, #65775, #17552, #39218, #60200, #22090, #12304, #59497, #32594, #17901, #6351, #60544, #27006, #43435, #33980, #59154, #53908, #43777, #11595, #6008, #32939, #49015, #54249, #65071, #17191, #38522, #59844, #66124, #7396, #7750, #51089, #29091, #61576, #56335, #13692, #24519 ),
 .UNSPECIFIED., .F., .F.,
 ( 4, 2, 2, 2, 2, 2, 2, 2, 2, 2, 2, 2, 2, 2, 2, 2, 1, 2, 2, 2, 2, 2, 2, 2, 2, 2, 2, 2, 2, 2, 2, 2, 4 ),
 ( 0.000000000000000000, 0.03125000000000000000, 0.06250000000000000000, 0.09375000000000000000, 0.1250000000000000000, 0.1562500000000000000, 0.1875000000000000000, 0.2187500000000000000, 0.2500000000000000000, 0.2812500000000000000, 0.3125000000000000000, 0.3437500000000000000, 0.3750000000000000000, 0.4062500000000000000, 0.4375000000000000000, 0.4687500000000000000, 0.5000000000000000000, 0.5312500000000000000, 0.5625000000000000000, 0.5937500000000000000, 0.6250000000000000000, 0.6562500000000000000, 0.6875000000000000000, 0.7187500000000000000, 0.7500000000000000000, 0.7812500000000000000, 0.8125000000000000000, 0.8437500000000000000, 0.8750000000000000000, 0.9062500000000000000, 0.9375000000000000000, 0.9687500000000000000, 1.000000000000000000 ),
 .UNSPECIFIED. ) ;
#16999=CARTESIAN_POINT ( 'NONE',  ( 6.183730561998000752, -0.04522467425096000221, -1.614091090670999984 ) ) ;
#17041=CARTESIAN_POINT ( 'NONE',  ( 5.002606837613999602, -0.4199405305951999789, 1.440017343911000003 ) ) ;
#17062=CARTESIAN_POINT ( 'NONE',  ( 6.928451469095000093, -1.283620250890999959, 0.4753010861453000335 ) ) ;
#17120=ORIENTED_EDGE ( 'NONE', *, *, #18314, .T. ) ;
#17191=CARTESIAN_POINT ( 'NONE',  ( 5.485952324345468867, 0.4288768802937203417, -1.048267794080263604 ) ) ;
#17225=CARTESIAN_POINT ( 'NONE',  ( 4.364220016632000210, -0.2958825345050999922, -1.301287971988999814 ) ) ;
#17256=CARTESIAN_POINT ( 'NONE',  ( 5.173974669483000888, -0.6654033835843000677, 1.142600628630999982 ) ) ;
#17289=CARTESIAN_POINT ( 'NONE',  ( 1.700000000000000178, 0.000000000000000000, 0.000000000000000000 ) ) ;
#17299=CARTESIAN_POINT ( 'NONE',  ( 4.716442238856000557, 1.389484359140999992, -0.2752418227443999554 ) ) ;
#17341=VECTOR ( 'NONE', #41036, 1000.000000000000000 ) ;
#17353=CARTESIAN_POINT ( 'NONE',  ( 6.788702397400999899, 1.551976682437999910, -0.4457619964912000188 ) ) ;
#17552=CARTESIAN_POINT ( 'NONE',  ( 6.035344492469169708, 0.9622224758110548004, -0.5982748535759940811 ) ) ;
#17579=CARTESIAN_POINT ( 'NONE',  ( 4.579397794411000255, 0.8193957582319000288, 1.053447925930000029 ) ) ;
#17614=CARTESIAN_POINT ( 'NONE',  ( 5.167306792578000518, -1.056937757944000023, -1.220746830110999825 ) ) ;
#17625=AXIS2_PLACEMENT_3D ( 'NONE', #6886, #43962, #32436 ) ;
#17688=CARTESIAN_POINT ( 'NONE',  ( 6.548735035738999954, -1.228754840668000003, 0.9029015244175999655 ) ) ;
#17700=ADVANCED_FACE ( 'NONE', ( #58049 ), #54732, .T. ) ;
#17711=CARTESIAN_POINT ( 'NONE',  ( 6.558504020673000312, -0.8406263976572999619, -1.204107458873000081 ) ) ;
#17728=CARTESIAN_POINT ( 'NONE',  ( 5.377827132531639798, -0.3835239794964074300, 1.315189805302956927 ) ) ;
#17730=CARTESIAN_POINT ( 'NONE',  ( 6.555026506349999948, -1.500000000000000000, 0.000000000000000000 ) ) ;
#17744=CARTESIAN_POINT ( 'NONE',  ( 5.815443173017626144, 1.499999999999999778, 0.1963495408493654004 ) ) ;
#17879=CARTESIAN_POINT ( 'NONE',  ( 3.400000000000000355, 0.000000000000000000, 0.000000000000000000 ) ) ;
#17881=ORIENTED_EDGE ( 'NONE', *, *, #23214, .F. ) ;
#17901=CARTESIAN_POINT ( 'NONE',  ( 5.841441374307528633, -1.121062338676339865, -0.1678582702746748423 ) ) ;
#17904=DIRECTION ( 'NONE',  ( 1.000000000000000000, 0.000000000000000000, 0.000000000000000000 ) ) ;
#17923=EDGE_CURVE ( 'NONE', #54822, #34817, #1341, .T. ) ;
#17961=CARTESIAN_POINT ( 'NONE',  ( 5.822692947599000135, 1.526675769738000010, -0.5259243426933000176 ) ) ;
#17991=DIRECTION ( 'NONE',  ( 1.000000000000000000, 0.000000000000000000, 0.000000000000000000 ) ) ;
#17993=ORIENTED_EDGE ( 'NONE', *, *, #51651, .F. ) ;
#18009=ORIENTED_EDGE ( 'NONE', *, *, #46793, .F. ) ;
#18055=CARTESIAN_POINT ( 'NONE',  ( 5.449388989100000025, -1.346921469446999975, 0.5851709088685000948 ) ) ;
#18084=CARTESIAN_POINT ( 'NONE',  ( 5.982109839683626973, -0.9218200799623778030, 1.199500263597266914 ) ) ;
#18093=B_SPLINE_CURVE_WITH_KNOTS ( 'NONE', 3,
 ( #55559, #29697, #12912, #55209, #8009, #3097 ),
 .UNSPECIFIED., .F., .F.,
 ( 4, 2, 4 ),
 ( 0.000000000000000000, 0.5000000000000000000, 1.000000000000000000 ),
 .UNSPECIFIED. ) ;
#18127=ORIENTED_EDGE ( 'NONE', *, *, #40789, .F. ) ;
#18213=DIRECTION ( 'NONE',  ( 0.000000000000000000, -1.000000000000000000, 0.000000000000000000 ) ) ;
#18269=PLANE ( 'NONE',  #67761 ) ;
#18303=CARTESIAN_POINT ( 'NONE',  ( 5.599162447775000828, -0.8041423837011999476, 1.228772791746999937 ) ) ;
#18314=EDGE_CURVE ( 'NONE', #59129, #426, #10062, .T. ) ;
#18330=CARTESIAN_POINT ( 'NONE',  ( 4.815443173016668688, 1.499999999999999778, 0.1963495408493654004 ) ) ;
#18341=DIRECTION ( 'NONE',  ( 1.000000000000000000, 0.000000000000000000, 0.000000000000000000 ) ) ;
#18346=PLANE ( 'NONE',  #3714 ) ;
#18397=CARTESIAN_POINT ( 'NONE',  ( 5.600631947950999390, -0.1174666901181000006, -1.463806399069999875 ) ) ;
#18442=CARTESIAN_POINT ( 'NONE',  ( 6.899999438051000133, 1.266765207443000030, 0.8033093483900000109 ) ) ;
#18470=ORIENTED_EDGE ( 'NONE', *, *, #53310, .F. ) ;
#18613=ORIENTED_EDGE ( 'NONE', *, *, #59679, .T. ) ;
#18692=ORIENTED_EDGE ( 'NONE', *, *, #59255, .F. ) ;
#18726=ADVANCED_FACE ( 'NONE', ( #27046 ), #464, .T. ) ;
#18743=CARTESIAN_POINT ( 'NONE',  ( 6.126648365476000002, 1.250196283310000211, -0.4306799594067000081 ) ) ;
#18751=ORIENTED_EDGE ( 'NONE', *, *, #55200, .T. ) ;
#18807=ORIENTED_EDGE ( 'NONE', *, *, #53310, .T. ) ;
#18854=CARTESIAN_POINT ( 'NONE',  ( 6.346693173016666911, 1.310679582531385501, 0.7554284705563518720 ) ) ;
#18870=DIRECTION ( 'NONE',  ( -1.000000000000000000, 0.000000000000000000, 0.000000000000000000 ) ) ;
#18873=ADVANCED_FACE ( 'NONE', ( #63230 ), #25500, .T. ) ;
#18876=ADVANCED_FACE ( 'NONE', ( #15008 ), #1759, .F. ) ;
#18941=CARTESIAN_POINT ( 'NONE',  ( 5.486746727192667983, -1.006919573152101233, 1.157429495210549941 ) ) ;
#18953=CARTESIAN_POINT ( 'NONE',  ( 1.700000000000000178, 0.000000000000000000, 0.000000000000000000 ) ) ;
#19020=DIRECTION ( 'NONE',  ( 0.000000000000000000, 0.000000000000000000, 1.000000000000000000 ) ) ;
#19070=CARTESIAN_POINT ( 'NONE',  ( 6.198935906450000033, 0.002327316029692999642, 1.176084684120999979 ) ) ;
#19090=DIRECTION ( 'NONE',  ( -1.000000000000000000, 0.000000000000000000, 0.000000000000000000 ) ) ;
#19194=ORIENTED_EDGE ( 'NONE', *, *, #52475, .T. ) ;
#19275=CARTESIAN_POINT ( 'NONE',  ( 7.289711015751999312, -0.9708250560305000665, 0.5387387265405000347 ) ) ;
#19290=ORIENTED_EDGE ( 'NONE', *, *, #46095, .T. ) ;
#19417=CARTESIAN_POINT ( 'NONE',  ( 5.269604931988000729, 0.1309856596131999951, 1.229810997071999923 ) ) ;
#19433=CARTESIAN_POINT ( 'NONE',  ( 3.400000000000000355, 1.000000000000000000, 0.000000000000000000 ) ) ;
#19451=VECTOR ( 'NONE', #35760, 1000.000000000000114 ) ;
#19489=CARTESIAN_POINT ( 'NONE',  ( 6.921938604046592225, -0.09431034973223660633, 1.509148051328639051 ) ) ;
#19515=EDGE_LOOP ( 'NONE', ( #37981, #29948, #47193, #37334, #27242, #49896, #58719, #38044, #5910, #49344 ) ) ;
#19593=CARTESIAN_POINT ( 'NONE',  ( 4.965649514109999885, 0.1599529892900000139, 1.501782300629000089 ) ) ;
#19655=CARTESIAN_POINT ( 'NONE',  ( 7.289711015751999312, -0.9708250560305000665, 0.5387387265405000347 ) ) ;
#19668=CARTESIAN_POINT ( 'NONE',  ( 0.7000000000000000666, 0.5773502691895999739, -1.000000000000000000 ) ) ;
#19676=EDGE_CURVE ( 'NONE', #6824, #54765, #23535, .T. ) ;
#19688=DIRECTION ( 'NONE',  ( 0.000000000000000000, -1.000000000000000000, 0.000000000000000000 ) ) ;
#19716=CARTESIAN_POINT ( 'NONE',  ( 0.2000000000000000389, 2.149999999999999911, 1.476203897337000000E-12 ) ) ;
#19787=CARTESIAN_POINT ( 'NONE',  ( 5.438359839683999830, 0.7554284705563453217, 1.310679582531389276 ) ) ;
#19794=CARTESIAN_POINT ( 'NONE',  ( 5.313359839684166808, 1.310679582531387943, -0.7554284705563468760 ) ) ;
#19841=CARTESIAN_POINT ( 'NONE',  ( 5.169609839683333874, -0.1963495408493606265, -1.500000000000000222 ) ) ;
#19914=CARTESIAN_POINT ( 'NONE',  ( 6.972601553427999477, -1.175206010251000022, 0.8635533004969999649 ) ) ;
#19927=DIRECTION ( 'NONE',  ( 0.000000000000000000, -0.5000000000000169864, -0.8660254037844288266 ) ) ;
#19936=CARTESIAN_POINT ( 'NONE',  ( 5.649576767392000320, -1.375515609181000132, 0.5142804259679000234 ) ) ;
#20016=CARTESIAN_POINT ( 'NONE',  ( 5.105886958660000197, 1.045076633341000205, 0.4412723599748000214 ) ) ;
#20028=DIRECTION ( 'NONE',  ( 1.000000000000000000, 0.000000000000000000, 0.000000000000000000 ) ) ;
#20071=ORIENTED_EDGE ( 'NONE', *, *, #26270, .F. ) ;
#20105=CARTESIAN_POINT ( 'NONE',  ( 5.190649514109999529, 0.1165019947749000029, 1.093825345293000018 ) ) ;
#20164=CARTESIAN_POINT ( 'NONE',  ( 6.836538849395999762, 1.535441917290000013, -0.2442687810326999998 ) ) ;
#20195=ORIENTED_EDGE ( 'NONE', *, *, #27574, .T. ) ;
#20214=CARTESIAN_POINT ( 'NONE',  ( -0.2999999999999999889, -0.5773502691895999739, -1.000000000000000000 ) ) ;
#20348=EDGE_CURVE ( 'NONE', #34817, #44723, #63398, .T. ) ;
#20356=CARTESIAN_POINT ( 'NONE',  ( 4.900628625324999987, -0.6489656778686000438, -0.9304565553949000201 ) ) ;
#20393=ORIENTED_EDGE ( 'NONE', *, *, #63286, .T. ) ;
#20431=EDGE_CURVE ( 'NONE', #55564, #47308, #4187, .T. ) ;
#20476=CARTESIAN_POINT ( 'NONE',  ( 5.479592101182999997, -0.7872145294400999527, 1.288886465870000109 ) ) ;
#20477=CARTESIAN_POINT ( 'NONE',  ( 5.105026506350000659, -1.500000000000000000, 0.000000000000000000 ) ) ;
#20508=CARTESIAN_POINT ( 'NONE',  ( 6.849078002582999147, 0.7730190231004000490, -1.183954730321999937 ) ) ;
#20567=AXIS2_PLACEMENT_3D ( 'NONE', #14837, #4332, #56805 ) ;
#20632=ORIENTED_EDGE ( 'NONE', *, *, #59679, .F. ) ;
#20700=CARTESIAN_POINT ( 'NONE',  ( 4.398018765420999898, -1.272903806234000124, 0.08056657245258999622 ) ) ;
#20715=CARTESIAN_POINT ( 'NONE',  ( 0.2000000000000000389, -2.149999999999999911, 0.000000000000000000 ) ) ;
#20779=CARTESIAN_POINT ( 'NONE',  ( 6.261216479699999837, -0.6943539861719999484, 0.9492381903959000722 ) ) ;
#20834=CARTESIAN_POINT ( 'NONE',  ( 4.570855421957501719, -1.392841697040837046, 0.6432039759612279139 ) ) ;
#20855=CARTESIAN_POINT ( 'NONE',  ( 7.040196970683999744, 0.9502619346694000102, -0.6159082020391000167 ) ) ;
#20925=ORIENTED_EDGE ( 'NONE', *, *, #7479, .F. ) ;
#20944=EDGE_LOOP ( 'NONE', ( #7948, #53872, #42678, #15815, #25160 ) ) ;
#20946=CARTESIAN_POINT ( 'NONE',  ( 7.426446028809999156, -0.5209984338309999741, 1.392739681806999918 ) ) ;
#21005=CARTESIAN_POINT ( 'NONE',  ( 3.400000000000000355, 0.000000000000000000, 0.000000000000000000 ) ) ;
#21023=( GEOMETRIC_REPRESENTATION_CONTEXT ( 3 ) GLOBAL_UNCERTAINTY_ASSIGNED_CONTEXT ( ( #52767 ) ) GLOBAL_UNIT_ASSIGNED_CONTEXT ( ( #60580, #12339, #65811 ) ) REPRESENTATION_CONTEXT ( 'NONE', 'WORKASPACE' ) );
#21045=CARTESIAN_POINT ( 'NONE',  ( 4.740115987645999951, 0.5852149391565999448, 1.133269042695999929 ) ) ;
#21071=AXIS2_PLACEMENT_3D ( 'NONE', #22026, #42674, #63981 ) ;
#21080=EDGE_CURVE ( 'NONE', #6237, #50848, #368, .T. ) ;
#21107=CARTESIAN_POINT ( 'NONE',  ( 5.896693173016667622, 1.310679582531385279, 0.7554284705563519831 ) ) ;
#21126=CARTESIAN_POINT ( 'NONE',  ( 6.304962922411999848, 0.03531958898060999497, -1.468087261088999895 ) ) ;
#21163=CARTESIAN_POINT ( 'NONE',  ( 6.127943173016666911, -0.9218200799623714747, -1.199500263597270466 ) ) ;
#21196=CARTESIAN_POINT ( 'NONE',  ( 6.973780705993999796, 0.1816583604578000111, -1.117739201043999930 ) ) ;
#21282=CARTESIAN_POINT ( 'NONE',  ( 6.895243336750000118, -0.9527829703796000249, 0.9274460053021000849 ) ) ;
#21295=EDGE_LOOP ( 'NONE', ( #26699, #31829, #14173, #3610 ) ) ;
#21359=CARTESIAN_POINT ( 'NONE',  ( 4.412215258034844823, -0.5741934336287252139, -0.9653862342499147653 ) ) ;
#21382=CARTESIAN_POINT ( 'NONE',  ( 5.231322606809000852, -0.4388467025999000515, 1.020924588955999912 ) ) ;
#21391=CARTESIAN_POINT ( 'NONE',  ( 4.782109839683042374, 0.9218200799623742503, -1.199500263597268912 ) ) ;
#21394=DIRECTION ( 'NONE',  ( 1.000000000000000000, 0.000000000000000000, 0.000000000000000000 ) ) ;
#21409=CARTESIAN_POINT ( 'NONE',  ( 7.289711015751999312, -0.9708250560305000665, 0.5387387265405000347 ) ) ;
#21457=LINE ( 'NONE', #31970, #10993 ) ;
#21461=CARTESIAN_POINT ( 'NONE',  ( 6.434332659906999652, 0.8081923938199999657, -1.046566182397999922 ) ) ;
#21485=AXIS2_PLACEMENT_3D ( 'NONE', #14576, #47420, #63132 ) ;
#21503=CARTESIAN_POINT ( 'NONE',  ( 5.092749183302999860, -0.2523854654960999699, -1.393817212909000069 ) ) ;
#21523=EDGE_CURVE ( 'NONE', #40516, #6243, #25767, .T. ) ;
#21524=EDGE_LOOP ( 'NONE', ( #36129, #690, #45499, #40551 ) ) ;
#21536=CARTESIAN_POINT ( 'NONE',  ( 6.616621076168000215, -0.9842248689287999008, 0.9580517823941999689 ) ) ;
#21555=CARTESIAN_POINT ( 'NONE',  ( 6.860989938375000818, -0.07351275584480999881, 1.466703212027999914 ) ) ;
#21620=CARTESIAN_POINT ( 'NONE',  ( 7.028075866130000016, -0.8537514372841999988, -1.069914814413999826 ) ) ;
#21660=CARTESIAN_POINT ( 'NONE',  ( 5.784193173017583511, 1.460959015002474493, -0.3926218265389176953 ) ) ;
#21674=PRESENTATION_STYLE_ASSIGNMENT (( #11878 ) ) ;
#21707=DIRECTION ( 'NONE',  ( -1.000000000000000000, 0.000000000000000000, 0.000000000000000000 ) ) ;
#21708=ORIENTED_EDGE ( 'NONE', *, *, #35370, .F. ) ;
#21718=CARTESIAN_POINT ( 'NONE',  ( 4.148014736430999605, 0.6585737698315999866, 0.8810829645851999681 ) ) ;
#21744=CARTESIAN_POINT ( 'NONE',  ( 6.471626508332579242, 0.2400263920404566986, -1.106823019747933401 ) ) ;
#21753=PLANE ( 'NONE',  #33322 ) ;
#21772=CARTESIAN_POINT ( 'NONE',  ( 4.392853487642000232, 1.339550729022999986, -0.6343589122600999941 ) ) ;
#21802=CARTESIAN_POINT ( 'NONE',  ( 5.325217628334000253, -0.8655273653155000080, -0.9996707749736001292 ) ) ;
#21831=CARTESIAN_POINT ( 'NONE',  ( 6.371592353486001059, 1.499999999999999556, 0.3122588619777424968 ) ) ;
#21840=CARTESIAN_POINT ( 'NONE',  ( 6.096693173016666023, -1.310679582531386389, -0.7554284705563492075 ) ) ;
#21845=CARTESIAN_POINT ( 'NONE',  ( 4.408554738853999844, -0.8547558900528000603, 1.129519256798999782 ) ) ;
#21856=CARTESIAN_POINT ( 'NONE',  ( 4.536684337565999314, -1.006062275253510663, 1.158256468153602725 ) ) ;
#21897=CARTESIAN_POINT ( 'NONE',  ( 5.578758726594999828, -1.574491786429000006, -0.3581626104627999574 ) ) ;
#21964=CARTESIAN_POINT ( 'NONE',  ( 6.762665658289999548, -0.7882360144965000481, 0.7672747788395000157 ) ) ;
#22026=CARTESIAN_POINT ( 'NONE',  ( -0.2999999999999999889, 0.000000000000000000, 0.000000000000000000 ) ) ;
#22057=VECTOR ( 'NONE', #30930, 1000.000000000000000 ) ;
#22090=CARTESIAN_POINT ( 'NONE',  ( 5.938392933388340289, -0.2293779303045812012, -1.109941115710884274 ) ) ;
#22095=CARTESIAN_POINT ( 'NONE',  ( 7.200276434330572961, 0.06778569668683269434, 1.141021389174379230 ) ) ;
#22099=VECTOR ( 'NONE', #41540, 1000.000000000000000 ) ;
#22120=CARTESIAN_POINT ( 'NONE',  ( 4.608031265421999478, -0.9445219429904000430, 1.142243179664999886 ) ) ;
#22133=DIRECTION ( 'NONE',  ( 0.000000000000000000, 1.000000000000000000, 0.000000000000000000 ) ) ;
#22150=CARTESIAN_POINT ( 'NONE',  ( 6.635989938375000285, -0.06619345247263999643, 1.320670790275000117 ) ) ;
#22196=CARTESIAN_POINT ( 'NONE',  ( 5.263797794415999931, 1.304926942633999998, 0.5509913562316999247 ) ) ;
#22246=CARTESIAN_POINT ( 'NONE',  ( 6.032487603146999611, -1.512468930016000135, 0.5654847974100999375 ) ) ;
#22255=CARTESIAN_POINT ( 'NONE',  ( 6.105026506350000659, -1.500000000000000000, 0.000000000000000000 ) ) ;
#22277=FACE_OUTER_BOUND ( 'NONE', #31385, .T. ) ;
#22283=CARTESIAN_POINT ( 'NONE',  ( 5.950859839683750430, -0.3926218265389256890, 1.460959015002472050 ) ) ;
#22285=ORIENTED_EDGE ( 'NONE', *, *, #33055, .T. ) ;
#22308=ORIENTED_EDGE ( 'NONE', *, *, #40265, .T. ) ;
#22310=CARTESIAN_POINT ( 'NONE',  ( 7.127700263164999939, 0.7483242745035000310, -1.146132291880999743 ) ) ;
#22326=CYLINDRICAL_SURFACE ( 'NONE', #46649, 1.500000000000000000 ) ;
#22370=FILL_AREA_STYLE ('',( #32529 ) ) ;
#22425=CARTESIAN_POINT ( 'NONE',  ( 6.570886616771333344, -1.393043258182016686, 0.6426200619446901241 ) ) ;
#22435=CARTESIAN_POINT ( 'NONE',  ( 6.132296051549998239, 0.8934716322868129224, 0.6963138618532788149 ) ) ;
#22461=CARTESIAN_POINT ( 'NONE',  ( 5.142503212292999670, 0.8998068448443999889, 0.7742560839445998822 ) ) ;
#22493=CARTESIAN_POINT ( 'NONE',  ( 5.404173046211999676, -0.7698221690009998674, -0.8891327474049000035 ) ) ;
#22523=CARTESIAN_POINT ( 'NONE',  ( 4.888359839683332098, 0.7554284705563452107, 1.310679582531388609 ) ) ;
#22525=CARTESIAN_POINT ( 'NONE',  ( -0.2999999999999999889, -1.649999999999999911, 0.000000000000000000 ) ) ;
#22535=CARTESIAN_POINT ( 'NONE',  ( 5.126958905526000088, 0.3514838302171000017, -1.372182189413999831 ) ) ;
#22562=LINE ( 'NONE', #43904, #27064 ) ;
#22591=CARTESIAN_POINT ( 'NONE',  ( 6.407261061822000059, -0.8669997925267000083, 1.185259004083000001 ) ) ;
#22623=CARTESIAN_POINT ( 'NONE',  ( 5.919609839683875663, 0.1963495408493571848, 1.500000000000000666 ) ) ;
#22698=ORIENTED_EDGE ( 'NONE', *, *, #20348, .T. ) ;
#22750=B_SPLINE_CURVE_WITH_KNOTS ( 'NONE', 3,
 ( #54688, #43859, #64130, #28124, #37567, #37916, #58901, #48408, #21831, #59236 ),
 .UNSPECIFIED., .F., .F.,
 ( 4, 2, 2, 2, 4 ),
 ( 0.000000000000000000, 0.2500000000000000000, 0.5000000000000000000, 0.7500000000000000000, 1.000000000000000000 ),
 .UNSPECIFIED. ) ;
#22781=CARTESIAN_POINT ( 'NONE',  ( 6.406992135612348704, -0.6435990042915642473, -0.9328669330701386819 ) ) ;
#22811=CARTESIAN_POINT ( 'NONE',  ( 4.389380990064000621, -0.8613159615020000714, -0.6842232203413000091 ) ) ;
#22820=FILL_AREA_STYLE_COLOUR ( '', #61206 ) ;
#22843=CARTESIAN_POINT ( 'NONE',  ( 5.368964071046000264, 1.564645433990000001, 0.3990237390554000063 ) ) ;
#22936=CARTESIAN_POINT ( 'NONE',  ( 5.881244644296000246, 1.024801514603000063, 1.247845015360000032 ) ) ;
#22949=CARTESIAN_POINT ( 'NONE',  ( -0.2999999999999999889, -0.5773502691895999739, 1.000000000000000000 ) ) ;
#22986=ORIENTED_EDGE ( 'NONE', *, *, #25174, .F. ) ;
#23027=VECTOR ( 'NONE', #45813, 1000.000000000000000 ) ;
#23061=VECTOR ( 'NONE', #30967, 1000.000000000000114 ) ;
#23073=ORIENTED_EDGE ( 'NONE', *, *, #37864, .T. ) ;
#23078=CARTESIAN_POINT ( 'NONE',  ( 1.700000000000000178, 0.000000000000000000, 0.000000000000000000 ) ) ;
#23121=CARTESIAN_POINT ( 'NONE',  ( 3.400000000000000355, -1.000000000000000000, 0.000000000000000000 ) ) ;
#23124=EDGE_CURVE ( 'NONE', #27875, #44844, #35902, .T. ) ;
#23133=CARTESIAN_POINT ( 'NONE',  ( 6.552419474232656249, 1.065422820183789865, -0.3854643328078556919 ) ) ;
#23142=CARTESIAN_POINT ( 'NONE',  ( 5.452606837613999780, -0.4199405305951999789, 1.440017343911000003 ) ) ;
#23157=ORIENTED_EDGE ( 'NONE', *, *, #57431, .T. ) ;
#23162=AXIS2_PLACEMENT_3D ( 'NONE', #4877, #41606, #25866 ) ;
#23169=CARTESIAN_POINT ( 'NONE',  ( 4.542107630820832576, -1.500000000000000888, 0.2435150667312298567 ) ) ;
#23194=CARTESIAN_POINT ( 'NONE',  ( 5.066478153344000646, -1.481027812490000040, 0.6434334968688999457 ) ) ;
#23214=EDGE_CURVE ( 'NONE', #25719, #4446, #6366, .T. ) ;
#23280=B_SPLINE_CURVE_WITH_KNOTS ( 'NONE', 3,
 ( #64687, #64335, #5963, #4933, #59107, #380, #58418, #68906, #26619, #42357, #728, #42689, #42008, #31183, #31863, #52837, #5278, #21359, #31516 ),
 .UNSPECIFIED., .F., .F.,
 ( 4, 1, 1, 1, 1, 1, 1, 1, 1, 1, 1, 1, 1, 1, 1, 1, 4 ),
 ( 0.000000000000000000, 0.04500315983054108820, 0.1100028832174083232, 0.1750026066042755235, 0.2400023299912177610, 0.3050020533779163046, 0.3700017767648023370, 0.4350015001516882585, 0.5000012235385741244, 0.5650009469254601013, 0.6300006703123461893, 0.6950003936992321663, 0.7600001170861181432, 0.8249998404730040091, 0.8899995638597026915, 0.9549992872465886684, 1.000000000000000000 ),
 .UNSPECIFIED. ) ;
#23294=CARTESIAN_POINT ( 'NONE',  ( 5.795621349514000542, -1.101608967510000037, 0.4118716830840000176 ) ) ;
#23326=FACE_OUTER_BOUND ( 'NONE', #34270, .T. ) ;
#23335=CARTESIAN_POINT ( 'NONE',  ( 6.801647950796354536, 1.188027738384418219, -0.9443810485859288617 ) ) ;
#23336=CARTESIAN_POINT ( 'NONE',  ( -0.2999999999999999889, -0.5773502691895999739, -1.000000000000000000 ) ) ;
#23337=CARTESIAN_POINT ( 'NONE',  ( 0.7000000000000000666, 0.000000000000000000, -0.5999999999999999778 ) ) ;
#23416=VERTEX_POINT ( 'NONE', #66139 ) ;
#23426=ORIENTED_EDGE ( 'NONE', *, *, #11200, .T. ) ;
#23487=DIRECTION ( 'NONE',  ( 0.000000000000000000, 0.000000000000000000, 1.000000000000000000 ) ) ;
#23535=CIRCLE ( 'NONE', #14609, 1.000000000000000000 ) ;
#23538=CARTESIAN_POINT ( 'NONE',  ( 5.800819726243000574, -0.04112960214766999550, -1.467935932961000001 ) ) ;
#23629=AXIS2_PLACEMENT_3D ( 'NONE', #37502, #25987, #68620 ) ;
#23633=CARTESIAN_POINT ( 'NONE',  ( 6.098107267216000160, 1.122942780917999928, 0.3495427174121999991 ) ) ;
#23636=FACE_OUTER_BOUND ( 'NONE', #33851, .T. ) ;
#23676=CARTESIAN_POINT ( 'NONE',  ( 6.838517237264255755, 1.484920755282000515, -0.3138429810103637307 ) ) ;
#23722=CIRCLE ( 'NONE', #58346, 0.5999999999999999778 ) ;
#23745=CARTESIAN_POINT ( 'NONE',  ( 6.305026506349999948, 1.500000000000000000, 0.000000000000000000 ) ) ;
#23782=CARTESIAN_POINT ( 'NONE',  ( 5.317324867288666823, 1.499999999999999778, 0.2318186422567637683 ) ) ;
#23787=ORIENTED_EDGE ( 'NONE', *, *, #25108, .T. ) ;
#23855=CARTESIAN_POINT ( 'NONE',  ( 4.260103625319000109, 0.7126091724783999437, -1.465752069756999898 ) ) ;
#23958=DIRECTION ( 'NONE',  ( 0.000000000000000000, 1.000000000000000000, 0.000000000000000000 ) ) ;
#23961=CARTESIAN_POINT ( 'NONE',  ( -0.2999999999999999889, 0.000000000000000000, 0.000000000000000000 ) ) ;
#23971=DIRECTION ( 'NONE',  ( 0.000000000000000000, 1.000000000000000000, 0.000000000000000000 ) ) ;
#23979=CARTESIAN_POINT ( 'NONE',  ( 5.521676530072999967, -0.1057711097905999903, -1.318062398728999884 ) ) ;
#24096=CARTESIAN_POINT ( 'NONE',  ( 7.399999923048000028, 0.000000000000000000, 0.000000000000000000 ) ) ;
#24163=ORIENTED_EDGE ( 'NONE', *, *, #8215, .F. ) ;
#24180=CARTESIAN_POINT ( 'NONE',  ( 5.469676782403334769, -0.7288346947182943181, 1.349937054441817219 ) ) ;
#24213=DIRECTION ( 'NONE',  ( 1.000000000000000000, 0.000000000000000000, 0.000000000000000000 ) ) ;
#24225=ADVANCED_FACE ( 'NONE', ( #8120, #7774 ), #18269, .T. ) ;
#24255=CARTESIAN_POINT ( 'NONE',  ( 4.971693173016667799, -0.7554284705563540925, 1.310679582531384391 ) ) ;
#24256=VERTEX_POINT ( 'NONE', #56707 ) ;
#24273=AXIS2_PLACEMENT_3D ( 'NONE', #23078, #44426, #2447 ) ;
#24274=CARTESIAN_POINT ( 'NONE',  ( 4.400048358572151486, 0.2121380062687552304, 1.494606510256098364 ) ) ;
#24324=CARTESIAN_POINT ( 'NONE',  ( 5.320019251605000221, -0.6654033835843000677, 1.142600628630999982 ) ) ;
#24356=ADVANCED_FACE ( 'NONE', ( #9141 ), #55509, .T. ) ;
#24359=VERTEX_POINT ( 'NONE', #51792 ) ;
#24376=CARTESIAN_POINT ( 'NONE',  ( 7.150000208772000043, 0.000000000000000000, 0.000000000000000000 ) ) ;
#24423=CARTESIAN_POINT ( 'NONE',  ( 6.605026506349999771, -1.500000000000000000, 0.000000000000000000 ) ) ;
#24439=CARTESIAN_POINT ( 'NONE',  ( 6.450859839683333874, -0.3926218265389256890, 1.460959015002472050 ) ) ;
#24519=CARTESIAN_POINT ( 'NONE',  ( 5.227606837614000135, -0.3108367803229999948, 1.065889863396000115 ) ) ;
#24520=CYLINDRICAL_SURFACE ( 'NONE', #14355, 1.500000000000000000 ) ;
#24551=B_SPLINE_CURVE_WITH_KNOTS ( 'NONE', 3,
 ( #36216, #57531, #4041, #19794, #25723, #41122, #52988, #31321, #35540, #5083, #35873, #3698, #25036, #9985, #63460, #68017, #41465, #20477 ),
 .UNSPECIFIED., .F., .F.,
 ( 4, 2, 2, 2, 2, 2, 2, 2, 4 ),
 ( 0.000000000000000000, 0.1250000000000000000, 0.2500000000000000000, 0.3750000000000000000, 0.5000000000000000000, 0.6250000000000000000, 0.7500000000000000000, 0.8750000000000000000, 1.000000000000000000 ),
 .UNSPECIFIED. ) ;
#24593=CARTESIAN_POINT ( 'NONE',  ( 6.627181666795220139, -0.9418933528413754308, -1.199469319010407542 ) ) ;
#24648=LINE ( 'NONE', #30247, #8425 ) ;
#24667=CARTESIAN_POINT ( 'NONE',  ( 5.572090849689999459, 0.6950325411885999172, -1.124902434106000104 ) ) ;
#24692=DIRECTION ( 'NONE',  ( 0.000000000000000000, 1.000000000000000000, 0.000000000000000000 ) ) ;
#24836=CARTESIAN_POINT ( 'NONE',  ( 5.296676530072999434, -0.1174666901181000006, -1.463806399069999875 ) ) ;
#24943=CARTESIAN_POINT ( 'NONE',  ( 5.013359839683332986, -1.310679582531389276, 0.7554284705563443225 ) ) ;
#24979=FACE_BOUND ( 'NONE', #43790, .T. ) ;
#24994=CARTESIAN_POINT ( 'NONE',  ( 6.160387840465999965, 0.6981053669911999604, 0.9464826977047000600 ) ) ;
#25030=CARTESIAN_POINT ( 'NONE',  ( 5.355026506350999860, 1.500000000000000000, 0.000000000000000000 ) ) ;
#25036=CARTESIAN_POINT ( 'NONE',  ( 5.177943173016958944, -0.9218200799623716968, -1.199500263597270910 ) ) ;
#25079=VERTEX_POINT ( 'NONE', #10438 ) ;
#25108=EDGE_CURVE ( 'NONE', #66643, #44271, #12591, .T. ) ;
#25144=CARTESIAN_POINT ( 'NONE',  ( 7.245399458952341831, -0.2246543155497662536, 1.160034907470290699 ) ) ;
#25154=CARTESIAN_POINT ( 'NONE',  ( 7.027948440668999375, -1.484077041169999944, -0.09315860241765000493 ) ) ;
#25160=ORIENTED_EDGE ( 'NONE', *, *, #67732, .T. ) ;
#25174=EDGE_CURVE ( 'NONE', #146, #49400, #9226, .T. ) ;
#25254=CARTESIAN_POINT ( 'NONE',  ( 4.490111958656000546, 0.5591895818894999648, -0.9870222206389998032 ) ) ;
#25336=CARTESIAN_POINT ( 'NONE',  ( 5.958730561998000219, -0.03293945794144000072, -1.175625617539999945 ) ) ;
#25370=CARTESIAN_POINT ( 'NONE',  ( 5.490443173017126810, -0.1963495408493673433, 1.499999999999999334 ) ) ;
#25378=DIRECTION ( 'NONE',  ( 1.000000000000000000, 0.000000000000000000, 0.000000000000000000 ) ) ;
#25410=CARTESIAN_POINT ( 'NONE',  ( 6.683037340858000164, -1.411194079024000070, -0.08858358730369000900 ) ) ;
#25491=CARTESIAN_POINT ( 'NONE',  ( 7.212165791352507682, 0.5478298943403082655, 1.085172144532685401 ) ) ;
#25500=CYLINDRICAL_SURFACE ( 'NONE', #43612, 1.500000000000000000 ) ;
#25544=ORIENTED_EDGE ( 'NONE', *, *, #66348, .T. ) ;
#25604=CARTESIAN_POINT ( 'NONE',  ( 4.295389598754000282, -0.2757437319869999737, 1.245290690854000015 ) ) ;
#25631=FACE_OUTER_BOUND ( 'NONE', #13334, .T. ) ;
#25644=CARTESIAN_POINT ( 'NONE',  ( 4.400041421715232381, -0.6049068342875222326, 1.258180343538149781 ) ) ;
#25719=VERTEX_POINT ( 'NONE', #10549 ) ;
#25722=CARTESIAN_POINT ( 'NONE',  ( 5.274333767848000676, 1.395439897136999896, -0.6918107995601999738 ) ) ;
#25723=CARTESIAN_POINT ( 'NONE',  ( 5.302943173017458989, 1.199500263597271799, -0.9218200799623701425 ) ) ;
#25728=VERTEX_POINT ( 'NONE', #10209 ) ;
#25758=CARTESIAN_POINT ( 'NONE',  ( 6.749453605548000112, -0.8819252889501000281, -1.105222071258000094 ) ) ;
#25767=CIRCLE ( 'NONE', #51428, 1.499999999999999334 ) ;
#25866=DIRECTION ( 'NONE',  ( 0.000000000000000000, 0.000000000000000000, -1.000000000000000000 ) ) ;
#25888=ORIENTED_EDGE ( 'NONE', *, *, #66348, .F. ) ;
#25918=EDGE_CURVE ( 'NONE', #44844, #27875, #49964, .T. ) ;
#25944=CARTESIAN_POINT ( 'NONE',  ( 4.534857654310999742, 0.1089978199666000042, -1.270785081792999982 ) ) ;
#25955=CARTESIAN_POINT ( 'NONE',  ( 0.2000000000000000389, 1.649999999999999911, 0.000000000000000000 ) ) ;
#25987=DIRECTION ( 'NONE',  ( -1.000000000000000000, 0.000000000000000000, 0.000000000000000000 ) ) ;
#26007=CARTESIAN_POINT ( 'NONE',  ( 5.969609839683333696, 0.1963495408493571015, 1.500000000000000444 ) ) ;
#26040=CARTESIAN_POINT ( 'NONE',  ( 5.543549751428999528, 1.090514925437999993, -0.4404064970261999945 ) ) ;
#26104=CARTESIAN_POINT ( 'NONE',  ( 7.002579511120999634, -0.5447379795254000401, 1.456200539209999922 ) ) ;
#26106=ORIENTED_EDGE ( 'NONE', *, *, #35370, .T. ) ;
#26155=LINE ( 'NONE', #20214, #22099 ) ;
#26202=UNCERTAINTY_MEASURE_WITH_UNIT (LENGTH_MEASURE( 1.000000000000000082E-05 ), #53159, 'distance_accuracy_value', 'NONE');
#26270=EDGE_CURVE ( 'NONE', #7001, #56519, #53304, .T. ) ;
#26283=ORIENTED_EDGE ( 'NONE', *, *, #3401, .T. ) ;
#26294=CARTESIAN_POINT ( 'NONE',  ( 5.174306403104999674, 0.3476685247999999895, 1.079832850831000002 ) ) ;
#26325=CARTESIAN_POINT ( 'NONE',  ( 6.805184800867738915, -1.078970173958359258, 0.3488539053363355902 ) ) ;
#26358=CARTESIAN_POINT ( 'NONE',  ( 5.990443173016668510, -0.1963495408493673433, 1.499999999999999334 ) ) ;
#26362=CARTESIAN_POINT ( 'NONE',  ( 4.399687792926640917, 1.101481271771440174, -0.7758419216000916885 ) ) ;
#26388=CARTESIAN_POINT ( 'NONE',  ( 5.644378390663000289, 0.7464156889442000731, 0.9088697504474000377 ) ) ;
#26412=CARTESIAN_POINT ( 'NONE',  ( 5.375859839684249408, 1.460959015002472494, 0.3926218265389233020 ) ) ;
#26414=CIRCLE ( 'NONE', #61048, 1.000000000000000000 ) ;
#26417=CARTESIAN_POINT ( 'NONE',  ( 4.941115032920667005, 0.7145727369020858921, 1.339076430445264032 ) ) ;
#26436=B_SPLINE_CURVE_WITH_KNOTS ( 'NONE', 3,
 ( #3806, #52048, #4151, #42269, #25491, #53091, #25144, #40883, #46819, #68124 ),
 .UNSPECIFIED., .F., .F.,
 ( 4, 2, 2, 2, 4 ),
 ( 0.000000000000000000, 0.2500000000000000000, 0.5000000000000000000, 0.7500000000000000000, 1.000000000000000000 ),
 .UNSPECIFIED. ) ;
#26450=CARTESIAN_POINT ( 'NONE',  ( 6.907364441304000735, -0.7063073661229000155, -0.8851390247125999755 ) ) ;
#26504=CARTESIAN_POINT ( 'NONE',  ( 7.084133413226945564, 0.1731109259882732954, -1.315866092581484459 ) ) ;
#26539=CARTESIAN_POINT ( 'NONE',  ( 6.928578894554999756, -1.109280206285000236, -0.5774939165396000273 ) ) ;
#26564=VECTOR ( 'NONE', #33627, 1000.000000000000000 ) ;
#26600=CARTESIAN_POINT ( 'NONE',  ( 0.7000000000000000666, -0.5773502691895999739, -1.000000000000000000 ) ) ;
#26616=EDGE_CURVE ( 'NONE', #54765, #24256, #12295, .T. ) ;
#26619=CARTESIAN_POINT ( 'NONE',  ( 4.867399517636808781, -1.067373159170256880, -0.5450599291056540396 ) ) ;
#26644=CARTESIAN_POINT ( 'NONE',  ( 4.979584043203000299, -0.7296458532426999266, -1.046132007313999912 ) ) ;
#26655=CARTESIAN_POINT ( 'NONE',  ( 4.834193173016584133, 1.460959015002474048, -0.3926218265389178064 ) ) ;
#26699=ORIENTED_EDGE ( 'NONE', *, *, #14931, .F. ) ;
#26725=CARTESIAN_POINT ( 'NONE',  ( 5.454587365828999168, -0.09407552946282000950, -1.172318398388999983 ) ) ;
#26769=CARTESIAN_POINT ( 'NONE',  ( 4.916518311043333256, 1.085476820253131081, 1.060886400888860548 ) ) ;
#26771=CARTESIAN_POINT ( 'NONE',  ( 4.384880990064000450, 0.9041977637900000531, 1.209694771924000101 ) ) ;
#26801=CARTESIAN_POINT ( 'NONE',  ( 6.948702399619000047, 1.366611866804000153, 0.3628763661032999854 ) ) ;
#26814=CARTESIAN_POINT ( 'NONE',  ( 5.294609839683333874, 1.500000000000001110, -0.1963495408493590721 ) ) ;
#26842=SHAPE_REPRESENTATION ( '510 Connector Pin', ( #9676 ), #67824 ) ;
#26884=CARTESIAN_POINT ( 'NONE',  ( 6.906312714198000080, -1.081792471387999832, 0.7949120843246000323 ) ) ;
#26922=ORIENTED_EDGE ( 'NONE', *, *, #5918, .T. ) ;
#26924=CARTESIAN_POINT ( 'NONE',  ( 5.732109839684041752, 0.9218200799623741393, -1.199500263597268690 ) ) ;
#26992=CARTESIAN_POINT ( 'NONE',  ( 4.709193173016083200, -0.3926218265389190276, -1.460959015002473826 ) ) ;
#27006=CARTESIAN_POINT ( 'NONE',  ( 5.776807001587030754, -0.8882760547343830915, 0.7026214500576545285 ) ) ;
#27011=CARTESIAN_POINT ( 'NONE',  ( 7.001027640260497620, 0.6248985950805467926, -0.9570937137488223501 ) ) ;
#27016=FACE_BOUND ( 'NONE', #60669, .T. ) ;
#27035=CARTESIAN_POINT ( 'NONE',  ( 4.554236820976999667, -0.02212662165366999917, 1.482009051976999947 ) ) ;
#27046=FACE_OUTER_BOUND ( 'NONE', #50277, .T. ) ;
#27051=CARTESIAN_POINT ( 'NONE',  ( 4.400000000000000355, -0.7080094843779000113, -0.8552562627201000245 ) ) ;
#27052=CARTESIAN_POINT ( 'NONE',  ( 4.669609839683333874, -0.1963495408493606265, -1.500000000000000222 ) ) ;
#27064=VECTOR ( 'NONE', #48798, 1000.000000000000000 ) ;
#27065=CARTESIAN_POINT ( 'NONE',  ( 5.627703546035999871, 0.07142731211511998968, 1.320368930804000085 ) ) ;
#27103=CARTESIAN_POINT ( 'NONE',  ( 6.305026506349999948, 1.500000000000000000, 0.000000000000000000 ) ) ;
#27108=CARTESIAN_POINT ( 'NONE',  ( 5.366426961083000435, -0.1673488337983000118, 1.406555471453999839 ) ) ;
#27153=VERTEX_POINT ( 'NONE', #7228 ) ;
#27160=CARTESIAN_POINT ( 'NONE',  ( 5.427515767744000463, 0.1599529892900000139, 1.501782300629000089 ) ) ;
#27216=CARTESIAN_POINT ( 'NONE',  ( 6.628782096734860296, -1.096045291018389101, 0.8220666491861405856 ) ) ;
#27220=ORIENTED_EDGE ( 'NONE', *, *, #47753, .F. ) ;
#27222=CARTESIAN_POINT ( 'NONE',  ( 7.161163246430999330, 0.5195473280092000046, 1.006186743336999978 ) ) ;
#27242=ORIENTED_EDGE ( 'NONE', *, *, #30074, .F. ) ;
#27244=EDGE_CURVE ( 'NONE', #53059, #24256, #26414, .T. ) ;
#27261=LINE ( 'NONE', #64298, #27339 ) ;
#27339=VECTOR ( 'NONE', #6618, 1000.000000000000114 ) ;
#27348=CARTESIAN_POINT ( 'NONE',  ( 6.714005406034039503, -0.1331244656375725477, 1.125151267359796536 ) ) ;
#27375=CARTESIAN_POINT ( 'NONE',  ( 4.661825709867000178, -1.451480533005000018, 0.3000752729519000073 ) ) ;
#27404=CARTESIAN_POINT ( 'NONE',  ( 5.303344406977999803, -1.078708783361999934, 0.4686457328678000356 ) ) ;
#27448=CARTESIAN_POINT ( 'NONE',  ( 5.310278024686999387, -0.4934046401541999360, 1.147847133074999748 ) ) ;
#27450=EDGE_CURVE ( 'NONE', #13866, #47471, #30904, .T. ) ;
#27501=CARTESIAN_POINT ( 'NONE',  ( 6.082901922763999991, -1.553728905769999891, -0.4396155223175000071 ) ) ;
#27508=CARTESIAN_POINT ( 'NONE',  ( 6.157109839683333696, -1.199500263597270022, -0.9218200799623730290 ) ) ;
#27566=CARTESIAN_POINT ( 'NONE',  ( 7.293740924889999810, 0.6280046043689999635, 1.216231657070000027 ) ) ;
#27574=EDGE_CURVE ( 'NONE', #6237, #31811, #16246, .T. ) ;
#27593=CARTESIAN_POINT ( 'NONE',  ( 5.855026506350000659, 1.500000000000000000, 0.000000000000000000 ) ) ;
#27647=B_SPLINE_CURVE_WITH_KNOTS ( 'NONE', 3,
 ( #13991, #23782, #2800, #28698, #51044, #61874, #39522, #55259, #12961, #45118 ),
 .UNSPECIFIED., .F., .F.,
 ( 4, 2, 2, 2, 4 ),
 ( 0.000000000000000000, 0.2500000000000000000, 0.5000000000000000000, 0.7500000000000000000, 1.000000000000000000 ),
 .UNSPECIFIED. ) ;
#27699=CARTESIAN_POINT ( 'NONE',  ( 6.164613237910274712, 0.5517680008132791469, 0.9902087497090418244 ) ) ;
#27704=CARTESIAN_POINT ( 'NONE',  ( 7.282019735819710071, -0.9188793378149595625, 0.6322026530472603101 ) ) ;
#27716=DIRECTION ( 'NONE',  ( 1.000000000000000000, 0.000000000000000000, 3.738339622219000240E-14 ) ) ;
#27729=CARTESIAN_POINT ( 'NONE',  ( 4.400000000000000355, 0.000000000000000000, 0.000000000000000000 ) ) ;
#27731=CARTESIAN_POINT ( 'NONE',  ( 4.905636958659999713, 1.235401976546000036, 1.063025361430000038 ) ) ;
#27760=B_SPLINE_CURVE_WITH_KNOTS ( 'NONE', 3,
 ( #43474, #15520, #36847, #31601, #5019, #52923, #53608, #43117, #26358, #26007, #47684, #64771, #16885, #11295, #21107, #32977, #37874, #4667 ),
 .UNSPECIFIED., .F., .F.,
 ( 4, 2, 2, 2, 2, 2, 2, 2, 4 ),
 ( 0.000000000000000000, 0.1250000000000000833, 0.2500000000000001665, 0.3750000000000001665, 0.5000000000000002220, 0.6250000000000002220, 0.7500000000000001110, 0.8750000000000001110, 1.000000000000000000 ),
 .UNSPECIFIED. ) ;
#27761=CARTESIAN_POINT ( 'NONE',  ( 5.757073283530000474, -0.6440133831468000114, 0.9840870706126000345 ) ) ;
#27791=CARTESIAN_POINT ( 'NONE',  ( 4.846693173016666911, 1.310679582531385501, 0.7554284705563518720 ) ) ;
#27805=CARTESIAN_POINT ( 'NONE',  ( 4.545393627743999687, -0.9903479682421998387, -1.012736759802999931 ) ) ;
#27851=B_SPLINE_CURVE_WITH_KNOTS ( 'NONE', 3,
 ( #44666, #17744, #7242, #971, #34168, #33477, #11443, #54792, #22623, #39064, #22283, #43624, #18084, #55139, #60726, #55486, #27889, #7586 ),
 .UNSPECIFIED., .F., .F.,
 ( 4, 2, 2, 2, 2, 2, 2, 2, 4 ),
 ( 0.000000000000000000, 0.1249999999999999722, 0.2499999999999999445, 0.3749999999999998890, 0.4999999999999998890, 0.6249999999999998890, 0.7499999999999997780, 0.8749999999999998890, 1.000000000000000000 ),
 .UNSPECIFIED. ) ;
#27854=CARTESIAN_POINT ( 'NONE',  ( 7.399999923048000028, 0.000000000000000000, -0.9999997023190999590 ) ) ;
#27857=CARTESIAN_POINT ( 'NONE',  ( 5.651046267567999770, 0.7718853692621999718, -1.249287881180999982 ) ) ;
#27875=VERTEX_POINT ( 'NONE', #53995 ) ;
#27889=CARTESIAN_POINT ( 'NONE',  ( 6.044609839683374730, -1.500000000000000444, 0.1963495408493560745 ) ) ;
#27891=ORIENTED_EDGE ( 'NONE', *, *, #27450, .F. ) ;
#27918=CARTESIAN_POINT ( 'NONE',  ( 7.194371378776000192, 0.06715535307189000880, 1.130410956850999904 ) ) ;
#27929=EDGE_LOOP ( 'NONE', ( #35959, #10414, #26922, #64608, #6102, #57472, #18751, #26106 ) ) ;
#27974=ORIENTED_EDGE ( 'NONE', *, *, #51709, .T. ) ;
#28009=CARTESIAN_POINT ( 'NONE',  ( 6.965816936038000229, -1.147328252452000097, 0.8605332073374000190 ) ) ;
#28024=DIRECTION ( 'NONE',  ( 0.000000000000000000, 1.000000000000000000, 0.000000000000000000 ) ) ;
#28043=CARTESIAN_POINT ( 'NONE',  ( 6.665529626493635895, 0.5345806894169679024, 0.9988415717975688279 ) ) ;
#28069=FACE_BOUND ( 'NONE', #50662, .T. ) ;
#28070=CARTESIAN_POINT ( 'NONE',  ( 4.981119878958000236, 0.2975160469921999673, -1.149139654934000054 ) ) ;
#28100=CARTESIAN_POINT ( 'NONE',  ( 6.276421824150999917, 0.9869232226998000401, -1.278013103562000152 ) ) ;
#28108=ORIENTED_EDGE ( 'NONE', *, *, #34465, .T. ) ;
#28124=CARTESIAN_POINT ( 'NONE',  ( 6.487553283437998530, -0.1491724392751367367, 1.524878087010347993 ) ) ;
#28173=CARTESIAN_POINT ( 'NONE',  ( 6.570873790634999878, -1.458001084847000195, 0.5398711174489000397 ) ) ;
#28193=CARTESIAN_POINT ( 'NONE',  ( 6.939945356251999264, -0.08083205921694999740, 1.612735633780000066 ) ) ;
#28208=DIRECTION ( 'NONE',  ( 0.000000000000000000, 1.000000000000000000, 0.000000000000000000 ) ) ;
#28222=CYLINDRICAL_SURFACE ( 'NONE', #17625, 1.500000000000000000 ) ;
#28237=CARTESIAN_POINT ( 'NONE',  ( 6.654170804923853488, -1.238391233191631802, -0.8776529624291122822 ) ) ;
#28274=ORIENTED_EDGE ( 'NONE', *, *, #25918, .T. ) ;
#28312=CIRCLE ( 'NONE', #61789, 1.000000000000000000 ) ;
#28385=B_SPLINE_CURVE_WITH_KNOTS ( 'NONE', 3,
 ( #23142, #24180, #18941, #66478, #44492, #59854 ),
 .UNSPECIFIED., .F., .F.,
 ( 4, 2, 4 ),
 ( 0.000000000000000000, 0.5000000000000000000, 1.000000000000000000 ),
 .UNSPECIFIED. ) ;
#28420=CARTESIAN_POINT ( 'NONE',  ( 4.658353212288999678, 0.7287915381420000394, 0.9369635204702000397 ) ) ;
#28515=AXIS2_PLACEMENT_3D ( 'NONE', #27729, #32289, #16532 ) ;
#28549=CARTESIAN_POINT ( 'NONE',  ( 6.703079102619000196, -0.05887414910050999678, 1.174638368522000098 ) ) ;
#28579=CYLINDRICAL_SURFACE ( 'NONE', #46479, 1.500000000000000000 ) ;
#28593=CARTESIAN_POINT ( 'NONE',  ( 6.727909377860130213, -0.04179919159915057580, -1.517065169120832779 ) ) ;
#28597=DIRECTION ( 'NONE',  ( 1.000000000000000000, 0.000000000000000000, 0.000000000000000000 ) ) ;
#28629=CARTESIAN_POINT ( 'NONE',  ( 1.700000000000000178, 0.000000000000000000, 0.000000000000000000 ) ) ;
#28647=DIRECTION ( 'NONE',  ( -1.000000000000000000, 0.000000000000000000, 0.000000000000000000 ) ) ;
#28660=CARTESIAN_POINT ( 'NONE',  ( 6.534193173016667799, -1.460959015002474493, 0.3926218265389144757 ) ) ;
#28698=CARTESIAN_POINT ( 'NONE',  ( 5.354219950104666559, 1.237977404532700332, 0.8781525088298994808 ) ) ;
#28713=ORIENTED_EDGE ( 'NONE', *, *, #27244, .T. ) ;
#28806=CARTESIAN_POINT ( 'NONE',  ( 5.750405406626000193, -0.9021507525358000157, -1.158728426834999992 ) ) ;
#28816=FACE_BOUND ( 'NONE', #15076, .T. ) ;
#28903=CARTESIAN_POINT ( 'NONE',  ( 6.782034520496999619, -0.06619345247263999643, 1.320670790275000117 ) ) ;
#28947=CARTESIAN_POINT ( 'NONE',  ( 6.703329853547768558, -0.4976103889317664564, -1.434029154780907644 ) ) ;
#28981=FACE_OUTER_BOUND ( 'NONE', #63040, .T. ) ;
#28991=ORIENTED_EDGE ( 'NONE', *, *, #14931, .T. ) ;
#29091=CARTESIAN_POINT ( 'NONE',  ( 5.308207799363945156, -1.091870064679186347, 0.3013736060501072123 ) ) ;
#29133=ORIENTED_EDGE ( 'NONE', *, *, #29958, .F. ) ;
#29147=CARTESIAN_POINT ( 'NONE',  ( 5.721864308364999374, -0.04522467425096000221, -1.614091090670999984 ) ) ;
#29241=CARTESIAN_POINT ( 'NONE',  ( 5.286409705193999997, -0.1287196877685000129, 1.257471894813999791 ) ) ;
#29359=CARTESIAN_POINT ( 'NONE',  ( 5.205914323403000310, 0.3864793456783000014, -1.508803618046000272 ) ) ;
#29437=ORIENTED_EDGE ( 'NONE', *, *, #63908, .T. ) ;
#29485=CARTESIAN_POINT ( 'NONE',  ( 6.778816671981999775, -0.8882170986559999593, 0.6661914818925001036 ) ) ;
#29514=B_SPLINE_CURVE_WITH_KNOTS ( 'NONE', 3,
 ( #60710, #17728, #60022, #12132 ),
 .UNSPECIFIED., .F., .F.,
 ( 4, 4 ),
 ( 0.000000000000000000, 1.000000000000000000 ),
 .UNSPECIFIED. ) ;
#29529=CARTESIAN_POINT ( 'NONE',  ( 4.940443173016666023, -0.1963495408493673156, 1.499999999999999556 ) ) ;
#29535=CIRCLE ( 'NONE', #57393, 2.149999999999999911 ) ;
#29582=CARTESIAN_POINT ( 'NONE',  ( 1.700000000000000178, 0.000000000000000000, 0.000000000000000000 ) ) ;
#29592=CARTESIAN_POINT ( 'NONE',  ( 6.047692947599000668, 1.111956540095999868, -0.3830577677631999967 ) ) ;
#29682=FACE_OUTER_BOUND ( 'NONE', #58047, .T. ) ;
#29689=CARTESIAN_POINT ( 'NONE',  ( 6.553816671982000130, -1.199981415667000118, 0.9000247785775999931 ) ) ;
#29697=CARTESIAN_POINT ( 'NONE',  ( 5.087956561560668334, -1.500000000000001110, 0.3217608788839214085 ) ) ;
#29706=CARTESIAN_POINT ( 'NONE',  ( 6.409193173016666911, 0.3926218265389159745, 1.460959015002474493 ) ) ;
#29746=ORIENTED_EDGE ( 'NONE', *, *, #64503, .F. ) ;
#29788=VECTOR ( 'NONE', #28208, 1000.000000000000000 ) ;
#29813=CARTESIAN_POINT ( 'NONE',  ( 4.313898069763999921, 1.472923203709999962, -0.6975189077233999724 ) ) ;
#29837=CARTESIAN_POINT ( 'NONE',  ( 7.156776345353000224, 1.243223188895000053, 2.274921040069000118E-10 ) ) ;
#29915=CARTESIAN_POINT ( 'NONE',  ( 5.055026506350000837, -1.500000000000000000, 0.000000000000000000 ) ) ;
#29933=CARTESIAN_POINT ( 'NONE',  ( 6.753493422235999688, -0.7428381837956999911, 0.9117187782023999931 ) ) ;
#29948=ORIENTED_EDGE ( 'NONE', *, *, #17923, .F. ) ;
#29958=EDGE_CURVE ( 'NONE', #6824, #53059, #4372, .T. ) ;
#29982=STYLED_ITEM ( 'NONE', ( #32974 ), #52451 ) ;
#29985=B_SPLINE_CURVE_WITH_KNOTS ( 'NONE', 3,
 ( #43540, #543, #20834, #21856, #11031, #10339, #42169, #33047, #54015, #63468 ),
 .UNSPECIFIED., .F., .F.,
 ( 4, 2, 2, 2, 4 ),
 ( 0.000000000000000000, 0.2500000000000000000, 0.5000000000000000000, 0.7500000000000000000, 1.000000000000000000 ),
 .UNSPECIFIED. ) ;
#30001=CARTESIAN_POINT ( 'NONE',  ( 6.965816936038000229, -1.147328252452000097, 0.8605332073374000190 ) ) ;
#30023=ORIENTED_EDGE ( 'NONE', *, *, #39500, .T. ) ;
#30033=FACE_OUTER_BOUND ( 'NONE', #59270, .T. ) ;
#30055=ORIENTED_EDGE ( 'NONE', *, *, #67260, .F. ) ;
#30074=EDGE_CURVE ( 'NONE', #66643, #7462, #16965, .T. ) ;
#30150=CARTESIAN_POINT ( 'NONE',  ( 4.421486958654000432, 1.000604198411000123, 1.286416736850999998 ) ) ;
#30192=CARTESIAN_POINT ( 'NONE',  ( 6.756521017669194329, 1.248225365452464652, -0.8739435346021212636 ) ) ;
#30205=CARTESIAN_POINT ( 'NONE',  ( 5.034193173016665135, -1.460959015002474493, 0.3926218265389144757 ) ) ;
#30247=CARTESIAN_POINT ( 'NONE',  ( 0.7000000000000000666, -0.5773502691895999739, 1.000000000000000000 ) ) ;
#30282=DIRECTION ( 'NONE',  ( 1.000000000000000000, 0.000000000000000000, 0.000000000000000000 ) ) ;
#30329=ORIENTED_EDGE ( 'NONE', *, *, #5034, .F. ) ;
#30342=CARTESIAN_POINT ( 'NONE',  ( 5.055026506350000837, -1.500000000000000000, 0.000000000000000000 ) ) ;
#30410=CARTESIAN_POINT ( 'NONE',  ( 7.127572837703999298, -0.3768015417652000321, -1.438462408934000125 ) ) ;
#30432=CARTESIAN_POINT ( 'NONE',  ( 5.520207029896999629, -0.8842068839782000200, 1.351115652313999771 ) ) ;
#30437=ORIENTED_EDGE ( 'NONE', *, *, #56041, .F. ) ;
#30468=CARTESIAN_POINT ( 'NONE',  ( -0.2999999999999999889, 0.5773502691895999739, -1.000000000000000000 ) ) ;
#30550=CARTESIAN_POINT ( 'NONE',  ( 4.400040034343773776, -0.7410138808234234542, 1.163549719693206974 ) ) ;
#30582=LINE ( 'NONE', #29915, #22057 ) ;
#30588=CARTESIAN_POINT ( 'NONE',  ( 6.798969222281000313, -1.006517980596000061, 0.5009083264753000364 ) ) ;
#30662=CARTESIAN_POINT ( 'NONE',  ( 6.828409023426000424, -0.7941163275365998864, -0.9951805479851000280 ) ) ;
#30677=CARTESIAN_POINT ( 'NONE',  ( 5.075859839683335650, -1.460959015002473826, -0.3926218265389207485 ) ) ;
#30688=ORIENTED_EDGE ( 'NONE', *, *, #3397, .F. ) ;
#30750=DIRECTION ( 'NONE',  ( 1.000000000000000000, 0.000000000000000000, 0.000000000000000000 ) ) ;
#30763=LINE ( 'NONE', #4177, #61860 ) ;
#30852=CARTESIAN_POINT ( 'NONE',  ( 5.013793765425000437, -0.2272566865862999941, -1.255041691444999996 ) ) ;
#30872=CARTESIAN_POINT ( 'NONE',  ( 6.742149978683131373, 1.067472389103388153, -1.089157552026253306 ) ) ;
#30885=CARTESIAN_POINT ( 'NONE',  ( 4.950859839683333874, -0.3926218265389256890, 1.460959015002472050 ) ) ;
#30903=DIRECTION ( 'NONE',  ( 1.000000000000000000, 0.000000000000000000, 3.219646771391999928E-14 ) ) ;
#30904=CIRCLE ( 'NONE', #65474, 2.149999999999999911 ) ;
#30930=DIRECTION ( 'NONE',  ( 1.000000000000000000, 0.000000000000000000, 0.000000000000000000 ) ) ;
#30934=CARTESIAN_POINT ( 'NONE',  ( -0.2999999999999999889, -1.154700538379000108, 0.000000000000000000 ) ) ;
#30967=DIRECTION ( 'NONE',  ( 0.000000000000000000, -0.5000000000000169864, -0.8660254037844288266 ) ) ;
#30979=CARTESIAN_POINT ( 'NONE',  ( 4.855026506350000659, 1.500000000000000000, 0.000000000000000000 ) ) ;
#31010=( GEOMETRIC_REPRESENTATION_CONTEXT ( 3 ) GLOBAL_UNCERTAINTY_ASSIGNED_CONTEXT ( ( #26202 ) ) GLOBAL_UNIT_ASSIGNED_CONTEXT ( ( #53159, #38103, #37763 ) ) REPRESENTATION_CONTEXT ( 'NONE', 'WORKASPACE' ) );
#31015=CARTESIAN_POINT ( 'NONE',  ( 6.994449685151000295, 1.257374890127000100, -0.2000319440639999891 ) ) ;
#31030=CARTESIAN_POINT ( 'NONE',  ( 5.107109839683333874, -1.199500263597270244, -0.9218200799623728070 ) ) ;
#31098=EDGE_CURVE ( 'NONE', #50848, #52040, #30763, .T. ) ;
#31103=CARTESIAN_POINT ( 'NONE',  ( 7.360029764120000095, 0.6822332425488999430, 1.321254113936999985 ) ) ;
#31133=ORIENTED_EDGE ( 'NONE', *, *, #23124, .F. ) ;
#31183=CARTESIAN_POINT ( 'NONE',  ( 4.598427295411807059, 1.165904589046791173, 0.2775696827697649582 ) ) ;
#31206=CARTESIAN_POINT ( 'NONE',  ( 4.250643903098000109, -0.6845482139417999878, 0.9045979078395999240 ) ) ;
#31281=CARTESIAN_POINT ( 'NONE',  ( 6.714945356252000508, -0.05887414910050999678, 1.174638368522000098 ) ) ;
#31305=CARTESIAN_POINT ( 'NONE',  ( 7.399999923048000028, 0.000000000000000000, 0.000000000000000000 ) ) ;
#31321=CARTESIAN_POINT ( 'NONE',  ( 5.250859839683916341, 0.3926218265389220807, -1.460959015002473382 ) ) ;
#31339=ORIENTED_EDGE ( 'NONE', *, *, #6126, .T. ) ;
#31353=CARTESIAN_POINT ( 'NONE',  ( 7.035787643465999608, -1.088193288857000063, 1.110433857983999850 ) ) ;
#31385=EDGE_LOOP ( 'NONE', ( #36278, #8778, #64205, #62687 ) ) ;
#31397=DIRECTION ( 'NONE',  ( 1.000000000000000000, 0.000000000000000000, 0.000000000000000000 ) ) ;
#31453=EDGE_CURVE ( 'NONE', #54265, #2358, #43608, .T. ) ;
#31458=ORIENTED_EDGE ( 'NONE', *, *, #9736, .T. ) ;
#31475=DIRECTION ( 'NONE',  ( -0.7071070235446059726, -0.7071065388284060171, -2.367528967094019852E-10 ) ) ;
#31483=DIRECTION ( 'NONE',  ( 1.000000000000000000, 0.000000000000000000, 0.000000000000000000 ) ) ;
#31516=CARTESIAN_POINT ( 'NONE',  ( 4.400000000000000355, -0.7080094843779000113, -0.8552562627201000245 ) ) ;
#31540=CARTESIAN_POINT ( 'NONE',  ( 5.082213209869999915, 0.8026392371705000084, -0.9912343320891000564 ) ) ;
#31571=CARTESIAN_POINT ( 'NONE',  ( 7.067443904950497569, 1.128838519570273258, -0.1795834841119597070 ) ) ;
#31591=DIRECTION ( 'NONE',  ( -1.000000000000000000, 0.000000000000000000, 0.000000000000000000 ) ) ;
#31601=CARTESIAN_POINT ( 'NONE',  ( 6.063359839683333696, -1.310679582531389498, 0.7554284705563444335 ) ) ;
#31605=CARTESIAN_POINT ( 'NONE',  ( 4.399785476046610633, -0.5075215790221194734, -1.032760291147674314 ) ) ;
#31660=VECTOR ( 'NONE', #4846, 1000.000000000000000 ) ;
#31696=CARTESIAN_POINT ( 'NONE',  ( 6.761992758735999587, -1.270688428506000056, -0.07976375540076000026 ) ) ;
#31763=EDGE_CURVE ( 'NONE', #37125, #24359, #11754, .T. ) ;
#31783=CARTESIAN_POINT ( 'NONE',  ( 6.828954497519999833, -0.8705094924380000210, 0.8473603920708000503 ) ) ;
#31811=VERTEX_POINT ( 'NONE', #60700 ) ;
#31816=PRODUCT_DEFINITION_FORMATION_WITH_SPECIFIED_SOURCE ( 'ANY', '', #56743, .NOT_KNOWN. ) ;
#31817=ORIENTED_EDGE ( 'NONE', *, *, #20431, .T. ) ;
#31829=ORIENTED_EDGE ( 'NONE', *, *, #33312, .T. ) ;
#31851=CARTESIAN_POINT ( 'NONE',  ( -0.2999999999999999889, 1.154700538379000108, 0.000000000000000000 ) ) ;
#31863=CARTESIAN_POINT ( 'NONE',  ( 4.544632850966807247, 1.083163139203730418, -0.5129437623365981080 ) ) ;
#31890=CARTESIAN_POINT ( 'NONE',  ( 4.969048069769999465, 0.2814927992946000268, -1.098939332150999926 ) ) ;
#31899=CARTESIAN_POINT ( 'NONE',  ( 4.855026506350000659, 1.500000000000000000, 0.000000000000000000 ) ) ;
#31914=AXIS2_PLACEMENT_3D ( 'NONE', #65036, #21707, #54569 ) ;
#31926=ORIENTED_EDGE ( 'NONE', *, *, #57431, .F. ) ;
#31949=CARTESIAN_POINT ( 'NONE',  ( 0.2000000000000000389, 0.000000000000000000, 0.000000000000000000 ) ) ;
#31953=CARTESIAN_POINT ( 'NONE',  ( 4.399647091626817996, 1.427585134858555760, -0.03664101042030128152 ) ) ;
#31955=CARTESIAN_POINT ( 'NONE',  ( 4.794609839683333874, 1.500000000000001110, -0.1963495408493590721 ) ) ;
#31970=CARTESIAN_POINT ( 'NONE',  ( 5.555026506349999948, -1.500000000000000000, 0.000000000000000000 ) ) ;
#31974=CARTESIAN_POINT ( 'NONE',  ( 6.103305643943999215, -0.8669997925267000083, 1.185259004083000001 ) ) ;
#32017=CARTESIAN_POINT ( 'NONE',  ( 5.229588072192999704, 1.415830339355000023, -0.04300091695264000174 ) ) ;
#32046=CARTESIAN_POINT ( 'NONE',  ( 7.106613235374000581, 1.094478228765999983, 0.2906167377007999875 ) ) ;
#32072=AXIS2_PLACEMENT_3D ( 'NONE', #45305, #12800, #23971 ) ;
#32131=B_SPLINE_SURFACE_WITH_KNOTS ( 'NONE', 3, 3, ( 
 ( #38550, #16189, #37513, #22461, #12333, #65102, #28070, #11978, #49734, #7080, #42762, #49379, #28420, #64070, #1495, #6037, #58837, #53597, #22811 ),
 ( #1843, #10946, #44160, #43108, #11284, #65458, #64409, #32290, #33664, #1152, #803, #11625, #17579, #43806, #48702, #59184, #17225, #59873, #54982 ),
 ( #64757, #38907, #32623, #16534, #53934, #33318, #5693, #54634, #60229, #27375, #22120, #27035, #48348, #454, #21772, #37860, #16875, #38199, #59529 ),
 ( #32965, #54279, #6380, #27731, #49043, #56364, #55680, #65804, #34010, #3220, #39248, #8810, #30150, #8469, #29813, #23855, #34705, #2193, #44510 ) ),
 .UNSPECIFIED., .F., .F., .F.,
 ( 4, 4 ),
 ( 4, 1, 1, 1, 1, 1, 1, 1, 1, 1, 1, 1, 1, 1, 1, 1, 4 ),
 ( -0.02636945251836000231, 1.026369452518000047 ),
 ( -0.01067046919480000092, 0.02400855568828999878, 0.05868758057138000195, 0.09336660545446999471, 0.1280456303375999971, 0.1627246552206000063, 0.1974036801037000188, 0.2320827049868000036, 0.2667617298698999884, 0.3014407547529999731, 0.3361197796361000134, 0.3707988045191999982, 0.4054778294023000385, 0.4401568542853999677, 0.4748358791684000324, 0.5095149040515000172, 0.5441939289345999464 ),
 .UNSPECIFIED. ) ;
#32134=CARTESIAN_POINT ( 'NONE',  ( 7.415504076822000634, -1.167372168626999995, 0.6628743416906999197 ) ) ;
#32152=ORIENTED_EDGE ( 'NONE', *, *, #48885, .T. ) ;
#32176=CARTESIAN_POINT ( 'NONE',  ( 5.596693173016832112, -1.310679582531386389, -0.7554284705563492075 ) ) ;
#32189=ORIENTED_EDGE ( 'NONE', *, *, #19676, .F. ) ;
#32193=DIRECTION ( 'NONE',  ( 0.000000000000000000, 1.000000000000000000, 0.000000000000000000 ) ) ;
#32226=VECTOR ( 'NONE', #44456, 1000.000000000000000 ) ;
#32259=ORIENTED_EDGE ( 'NONE', *, *, #63286, .F. ) ;
#32289=DIRECTION ( 'NONE',  ( 1.000000000000000000, 0.000000000000000000, 0.000000000000000000 ) ) ;
#32290=CARTESIAN_POINT ( 'NONE',  ( 4.848370016636000202, -0.5474368957134999603, -1.217158087947000089 ) ) ;
#32315=CARTESIAN_POINT ( 'NONE',  ( 5.656244644296000601, 0.7464156889442000731, 0.9088697504474000377 ) ) ;
#32352=CARTESIAN_POINT ( 'NONE',  ( 6.232109839683333874, 0.9218200799623741393, -1.199500263597268690 ) ) ;
#32357=CARTESIAN_POINT ( 'NONE',  ( 4.829607378956000119, 1.514947213439000073, 0.3616484269658999939 ) ) ;
#32409=CARTESIAN_POINT ( 'NONE',  ( 6.003946504885999680, -1.413039514337999902, -0.3998085520867999954 ) ) ;
#32436=DIRECTION ( 'NONE',  ( 0.000000000000000000, -1.000000000000000000, 0.000000000000000000 ) ) ;
#32472=CARTESIAN_POINT ( 'NONE',  ( 7.094492130820000853, 0.2195801626521000083, -1.351071070713000033 ) ) ;
#32529=FILL_AREA_STYLE_COLOUR ( '', #37686 ) ;
#32545=ADVANCED_FACE ( 'NONE', ( #7842 ), #50149, .T. ) ;
#32594=CARTESIAN_POINT ( 'NONE',  ( 5.873758560667790007, -0.9662729582186857513, -0.5911492727768954403 ) ) ;
#32598=CARTESIAN_POINT ( 'NONE',  ( 3.350000000000000089, 0.000000000000000000, 0.000000000000000000 ) ) ;
#32623=CARTESIAN_POINT ( 'NONE',  ( 5.038386820982999836, 0.2713898421607000566, 1.457004540053999930 ) ) ;
#32634=DIRECTION ( 'NONE',  ( 0.000000000000000000, -1.000000000000000000, 0.000000000000000000 ) ) ;
#32652=CARTESIAN_POINT ( 'NONE',  ( 5.123560349866000507, 0.1309856596131999951, 1.229810997071999923 ) ) ;
#32694=CARTESIAN_POINT ( 'NONE',  ( 4.887490849967999651, -0.5294863075682000320, 1.313799488281000016 ) ) ;
#32747=CARTESIAN_POINT ( 'NONE',  ( 6.709746979523999677, 1.411445953971000034, -0.4053984660343999957 ) ) ;
#32757=CARTESIAN_POINT ( 'NONE',  ( 6.271693173016666734, 0.7554284705563509839, -1.310679582531385945 ) ) ;
#32812=CARTESIAN_POINT ( 'NONE',  ( 7.260660218006000477, 0.07416480754746999915, 1.248399527803000009 ) ) ;
#32832=EDGE_CURVE ( 'NONE', #4446, #25728, #29985, .T. ) ;
#32842=CARTESIAN_POINT ( 'NONE',  ( 5.646693173016667622, -1.310679582531386611, -0.7554284705563495406 ) ) ;
#32925=CARTESIAN_POINT ( 'NONE',  ( 6.305026506349999948, 1.500000000000000000, 0.000000000000000000 ) ) ;
#32939=CARTESIAN_POINT ( 'NONE',  ( 5.582903883426274305, 1.131774569182460111, 0.04058116965622569905 ) ) ;
#32965=CARTESIAN_POINT ( 'NONE',  ( 5.013225847549999337, -0.7131102322965999774, 1.331318456966000152 ) ) ;
#32974=PRESENTATION_STYLE_ASSIGNMENT (( #55335 ) ) ;
#32977=CARTESIAN_POINT ( 'NONE',  ( 5.875859839683334584, 1.460959015002472494, 0.3926218265389233020 ) ) ;
#32997=CARTESIAN_POINT ( 'NONE',  ( 6.657863159730999847, -1.329569516000000062, 0.3446834961110000206 ) ) ;
#33039=CARTESIAN_POINT ( 'NONE',  ( 4.555929601177000521, -1.554405035535000090, 0.09838377833599000477 ) ) ;
#33047=CARTESIAN_POINT ( 'NONE',  ( 4.434171084391500095, 0.8317986529663452533, 1.289119990005314520 ) ) ;
#33055=EDGE_CURVE ( 'NONE', #63838, #37303, #59527, .T. ) ;
#33058=ORIENTED_EDGE ( 'NONE', *, *, #36137, .T. ) ;
#33095=CARTESIAN_POINT ( 'NONE',  ( 6.306432422588000186, 0.8716839254852999375, 1.181818379215999970 ) ) ;
#33131=DIRECTION ( 'NONE',  ( 1.000000000000000000, 0.000000000000000000, 0.000000000000000000 ) ) ;
#33160=CARTESIAN_POINT ( 'NONE',  ( 7.194116527854999887, 1.351798952403999943, -0.2150535807229000118 ) ) ;
#33267=AXIS2_PLACEMENT_3D ( 'NONE', #25955, #52179, #47287 ) ;
#33268=DIRECTION ( 'NONE',  ( 1.000000000000000000, 0.000000000000000000, 0.000000000000000000 ) ) ;
#33312=EDGE_CURVE ( 'NONE', #56519, #41499, #67522, .T. ) ;
#33318=CARTESIAN_POINT ( 'NONE',  ( 4.877003487648000402, 1.187560281918999872, -0.8868741825288999348 ) ) ;
#33322=AXIS2_PLACEMENT_3D ( 'NONE', #94, #16514, #37842 ) ;
#33325=CARTESIAN_POINT ( 'NONE',  ( 4.555026506349999948, -1.500000000000000000, 0.000000000000000000 ) ) ;
#33348=CARTESIAN_POINT ( 'NONE',  ( 6.641058386525000579, -1.256780975885000151, 0.6254553495446000255 ) ) ;
#33384=CARTESIAN_POINT ( 'NONE',  ( 6.065443173016666911, -1.500000000000000222, -0.1963495408493622363 ) ) ;
#33441=CARTESIAN_POINT ( 'NONE',  ( 5.780416005063000462, 1.497237214918999859, -0.6046620561147000306 ) ) ;
#33464=LINE ( 'NONE', #17730, #38760 ) ;
#33477=CARTESIAN_POINT ( 'NONE',  ( 5.877943173017373901, 0.9218200799623692543, 1.199500263597272687 ) ) ;
#33482=ORIENTED_EDGE ( 'NONE', *, *, #51651, .T. ) ;
#33489=CARTESIAN_POINT ( 'NONE',  ( 6.629591280611910165, -1.445352440277137163, -0.4631782753073599990 ) ) ;
#33537=ORIENTED_EDGE ( 'NONE', *, *, #56098, .T. ) ;
#33578=FACE_OUTER_BOUND ( 'NONE', #13255, .T. ) ;
#33627=DIRECTION ( 'NONE',  ( 1.000000000000000000, 0.000000000000000000, 0.000000000000000000 ) ) ;
#33661=DIRECTION ( 'NONE',  ( 0.000000000000000000, -0.5000000000000169864, 0.8660254037844288266 ) ) ;
#33664=CARTESIAN_POINT ( 'NONE',  ( 4.794575572191000390, -1.188595002225999897, -0.6069625248515000404 ) ) ;
#33694=CARTESIAN_POINT ( 'NONE',  ( 5.055026506350000837, -1.500000000000000000, 0.000000000000000000 ) ) ;
#33770=CARTESIAN_POINT ( 'NONE',  ( 6.537665658289999904, -1.082219296144999898, 1.053440284172000085 ) ) ;
#33790=CARTESIAN_POINT ( 'NONE',  ( 6.839116717017999392, 1.514695785805999950, 0.5594970275663000425 ) ) ;
#33851=EDGE_LOOP ( 'NONE', ( #13598, #47186, #34099, #44600 ) ) ;
#33907=CARTESIAN_POINT ( 'NONE',  ( 7.399999923048000028, -0.9999997023190999590, 0.000000000000000000 ) ) ;
#33980=CARTESIAN_POINT ( 'NONE',  ( 5.728331222046617377, -0.3264931479727770647, 1.084430188123998828 ) ) ;
#34010=CARTESIAN_POINT ( 'NONE',  ( 4.636664736434999767, -1.451451435390000100, -0.7411915970320999136 ) ) ;
#34045=CARTESIAN_POINT ( 'NONE',  ( 6.427664783001999282, 0.8895447933473999980, 1.347595971237000256 ) ) ;
#34058=DIRECTION ( 'NONE',  ( -1.000000000000000000, 0.000000000000000000, 0.000000000000000000 ) ) ;
#34069=FACE_OUTER_BOUND ( 'NONE', #21524, .T. ) ;
#34099=ORIENTED_EDGE ( 'NONE', *, *, #9007, .F. ) ;
#34137=CARTESIAN_POINT ( 'NONE',  ( 5.773748128158000092, 0.07142731211511998968, 1.320368930804000085 ) ) ;
#34168=CARTESIAN_POINT ( 'NONE',  ( 5.857109839684125241, 1.199500263597268246, 0.9218200799623752495 ) ) ;
#34217=DIRECTION ( 'NONE',  ( 0.000000000000000000, -1.000000000000000000, 0.000000000000000000 ) ) ;
#34270=EDGE_LOOP ( 'NONE', ( #68866, #63580, #17881, #25544 ) ) ;
#34276=CIRCLE ( 'NONE', #4099, 1.500000000000000000 ) ;
#34367=AXIS2_PLACEMENT_3D ( 'NONE', #23961, #66602, #7529 ) ;
#34391=CARTESIAN_POINT ( 'NONE',  ( 6.478079102618999663, -0.08083205921694999740, 1.612735633780000066 ) ) ;
#34424=CARTESIAN_POINT ( 'NONE',  ( 4.857109839683332986, 1.199500263597268246, 0.9218200799623752495 ) ) ;
#34465=EDGE_CURVE ( 'NONE', #7462, #47308, #23280, .T. ) ;
#34490=CARTESIAN_POINT ( 'NONE',  ( 6.378719963561000128, -1.260983081135999884, 0.3979920142897999669 ) ) ;
#34514=DIRECTION ( 'NONE',  ( 1.000000000000000000, 0.000000000000000000, 0.000000000000000000 ) ) ;
#34547=CARTESIAN_POINT ( 'NONE',  ( 7.305862029444999628, -1.022267936763999963, 0.4061956009805000600 ) ) ;
#34548=B_SPLINE_CURVE_WITH_KNOTS ( 'NONE', 3,
 ( #42247, #26504, #63552, #58311, #58656, #5515, #37676, #6547, #49542, #65960 ),
 .UNSPECIFIED., .F., .F.,
 ( 4, 2, 2, 2, 4 ),
 ( 0.5000000021935380179, 0.6250000016451535689, 0.7500000010967690089, 0.8750000005483844490, 1.000000000000000000 ),
 .UNSPECIFIED. ) ;
#34601=CARTESIAN_POINT ( 'NONE',  ( 6.357109839683332986, 1.199500263597268246, 0.9218200799623752495 ) ) ;
#34615=EDGE_CURVE ( 'NONE', #68689, #58024, #5878, .T. ) ;
#34650=DIRECTION ( 'NONE',  ( 0.000000000000000000, -1.000000000000000000, 0.000000000000000000 ) ) ;
#34705=CARTESIAN_POINT ( 'NONE',  ( 4.206309180874000297, -0.3613166205557999944, -1.589066327271000167 ) ) ;
#34817=VERTEX_POINT ( 'NONE', #7614 ) ;
#34825=CARTESIAN_POINT ( 'NONE',  ( 6.277891324327000255, 0.002616650692276999927, 1.322296913527999829 ) ) ;
#34847=CARTESIAN_POINT ( 'NONE',  ( 5.563359839683501562, -1.310679582531389498, 0.7554284705563444335 ) ) ;
#34942=CARTESIAN_POINT ( 'NONE',  ( 5.069075434514000555, -1.549422555689000003, -0.1585698209677000037 ) ) ;
#34975=ADVANCED_FACE ( 'NONE', ( #13221 ), #54636, .F. ) ;
#34981=EDGE_LOOP ( 'NONE', ( #66450, #18692, #3594, #59487, #20632, #25888, #54224, #31817 ) ) ;
#35009=CARTESIAN_POINT ( 'NONE',  ( 4.625859839682417984, -1.460959015002473382, -0.3926218265389205819 ) ) ;
#35096=CARTESIAN_POINT ( 'NONE',  ( 1.700000000000000178, 1.500000000000000000, 0.000000000000000000 ) ) ;
#35169=CARTESIAN_POINT ( 'NONE',  ( 6.451007504533999182, 0.02828639361845000297, -1.175746811673999970 ) ) ;
#35216=ORIENTED_EDGE ( 'NONE', *, *, #3401, .F. ) ;
#35244=CARTESIAN_POINT ( 'NONE',  ( 5.065443173016666911, -1.500000000000000222, -0.1963495408493622363 ) ) ;
#35257=DIRECTION ( 'NONE',  ( -0.000000000000000000, 0.8660254037844288266, 0.5000000000000169864 ) ) ;
#35280=CARTESIAN_POINT ( 'NONE',  ( 6.377943173016666911, 0.9218200799623692543, 1.199500263597272687 ) ) ;
#35315=CARTESIAN_POINT ( 'NONE',  ( 7.393237896465000958, 0.08818371649832000558, 1.484376669706999996 ) ) ;
#35333=CARTESIAN_POINT ( 'NONE',  ( 0.2000000000000000389, -2.149999999999999911, -1.475903017541000135E-12 ) ) ;
#35370=EDGE_CURVE ( 'NONE', #56839, #65623, #43285, .T. ) ;
#35443=CARTESIAN_POINT ( 'NONE',  ( 5.044609839683332986, -1.500000000000000444, 0.1963495408493560745 ) ) ;
#35496=FACE_OUTER_BOUND ( 'NONE', #423, .T. ) ;
#35508=CARTESIAN_POINT ( 'NONE',  ( 6.227477004709999875, 0.7848946462383999956, 1.064150538460000073 ) ) ;
#35540=CARTESIAN_POINT ( 'NONE',  ( 5.240443173017209411, 0.1963495408493638184, -1.499999999999999778 ) ) ;
#35577=CARTESIAN_POINT ( 'NONE',  ( 7.077542425583873253, -1.465994342824544899E-06, -1.322443989608400816 ) ) ;
#35657=CARTESIAN_POINT ( 'NONE',  ( 7.260405367085000172, 1.468527740333999798, -0.2336236082946000214 ) ) ;
#35677=CARTESIAN_POINT ( 'NONE',  ( 6.024350226066000680, -0.9533226957039999672, 1.303269410926999994 ) ) ;
#35760=DIRECTION ( 'NONE',  ( 0.000000000000000000, 0.5000000000000169864, -0.8660254037844288266 ) ) ;
#35797=CARTESIAN_POINT ( 'NONE',  ( 4.400045583829395923, -0.1517171157701598105, 1.464984729050318846 ) ) ;
#35873=CARTESIAN_POINT ( 'NONE',  ( 5.209193173017084177, -0.3926218265389190276, -1.460959015002473826 ) ) ;
#35902=CIRCLE ( 'NONE', #23629, 0.5999999999999999778 ) ;
#35959=ORIENTED_EDGE ( 'NONE', *, *, #14195, .F. ) ;
#36008=EDGE_LOOP ( 'NONE', ( #59147, #20071, #54448, #8681 ) ) ;
#36010=CARTESIAN_POINT ( 'NONE',  ( 6.578907741853000424, -1.461948210420000116, 0.3790019357670000311 ) ) ;
#36041=CARTESIAN_POINT ( 'NONE',  ( 6.964951367667778115, 0.8867442030251825313, 1.153938778527312969 ) ) ;
#36091=CARTESIAN_POINT ( 'NONE',  ( 4.421692514211000180, -0.3829406755631999393, -1.067830647061000171 ) ) ;
#36129=ORIENTED_EDGE ( 'NONE', *, *, #40789, .T. ) ;
#36137=EDGE_CURVE ( 'NONE', #42702, #40516, #69019, .T. ) ;
#36206=CARTESIAN_POINT ( 'NONE',  ( 5.521693173017002465, -0.7554284705563544255, 1.310679582531384169 ) ) ;
#36209=AXIS2_PLACEMENT_3D ( 'NONE', #17289, #17991, #55390 ) ;
#36214=CARTESIAN_POINT ( 'NONE',  ( 5.376962934516001269, 1.051792491445999955, 1.148731044744000007 ) ) ;
#36216=CARTESIAN_POINT ( 'NONE',  ( 5.355026506350999860, 1.500000000000000000, 0.000000000000000000 ) ) ;
#36245=CARTESIAN_POINT ( 'NONE',  ( 6.785601289371999911, -0.8949653936606000171, 0.6576296519798999762 ) ) ;
#36254=VECTOR ( 'NONE', #33661, 1000.000000000000114 ) ;
#36278=ORIENTED_EDGE ( 'NONE', *, *, #18314, .F. ) ;
#36334=CARTESIAN_POINT ( 'NONE',  ( 7.481792916052000031, -1.268175574387999882, 0.7201140061520999724 ) ) ;
#36340=ORIENTED_EDGE ( 'NONE', *, *, #55577, .F. ) ;
#36346=VERTEX_POINT ( 'NONE', #3376 ) ;
#36379=CARTESIAN_POINT ( 'NONE',  ( 1.700000000000000178, 0.000000000000000000, 0.000000000000000000 ) ) ;
#36388=CARTESIAN_POINT ( 'NONE',  ( 7.224759086135252417, -0.7889424787723180454, 0.8956307892555190886 ) ) ;
#36433=CARTESIAN_POINT ( 'NONE',  ( 4.832209180879999622, -1.128524195065999880, -0.1154945620947999962 ) ) ;
#36461=CYLINDRICAL_SURFACE ( 'NONE', #5449, 1.000000000000000000 ) ;
#36483=B_SPLINE_CURVE_WITH_KNOTS ( 'NONE', 3,
 ( #68394, #36600, #19489, #14250, #51977, #30001 ),
 .UNSPECIFIED., .F., .F.,
 ( 4, 2, 4 ),
 ( 0.000000000000000000, 0.5000000000000000000, 1.000000000000000000 ),
 .UNSPECIFIED. ) ;
#36487=CARTESIAN_POINT ( 'NONE',  ( 6.899999438051000133, 0.000000000000000000, 0.000000000000000000 ) ) ;
#36502=CIRCLE ( 'NONE', #32072, 1.500000000000000000 ) ;
#36557=CARTESIAN_POINT ( 'NONE',  ( 4.904219950104667269, 1.237977404532700332, 0.8781525088298995918 ) ) ;
#36592=CARTESIAN_POINT ( 'NONE',  ( 7.215837234118000154, -1.085830440727999946, 0.6165721249222000377 ) ) ;
#36600=CARTESIAN_POINT ( 'NONE',  ( 6.910969021048729566, 0.2454124519544698679, 1.504446442354156366 ) ) ;
#36667=EDGE_CURVE ( 'NONE', #49026, #3750, #26436, .T. ) ;
#36684=DIRECTION ( 'NONE',  ( 0.000000000000000000, -1.000000000000000000, 0.000000000000000000 ) ) ;
#36730=DIRECTION ( 'NONE',  ( 1.000000000000000000, 0.000000000000000000, 0.000000000000000000 ) ) ;
#36785=CARTESIAN_POINT ( 'NONE',  ( 5.071677236438000058, 1.133895819062999966, -0.03443813753193999960 ) ) ;
#36806=ORIENTED_EDGE ( 'NONE', *, *, #23214, .T. ) ;
#36817=CARTESIAN_POINT ( 'NONE',  ( 7.100652037295501096, 1.104751383945007825, 0.2933445679723732380 ) ) ;
#36847=CARTESIAN_POINT ( 'NONE',  ( 6.084193173016664957, -1.460959015002474937, 0.3926218265389144757 ) ) ;
#36852=CARTESIAN_POINT ( 'NONE',  ( 4.732109839683332986, 0.9218200799623741393, -1.199500263597268690 ) ) ;
#36864=AXIS2_PLACEMENT_3D ( 'NONE', #52453, #36730, #5245 ) ;
#36880=CARTESIAN_POINT ( 'NONE',  ( 0.7000000000000000666, -1.154700538379000108, 0.000000000000000000 ) ) ;
#36907=CARTESIAN_POINT ( 'NONE',  ( 4.978010115736667629, 0.04029576578756273453, 1.517272597181324789 ) ) ;
#36943=CARTESIAN_POINT ( 'NONE',  ( 6.795200891081000449, -1.129313230629999998, -0.5879231567111999901 ) ) ;
#36970=CARTESIAN_POINT ( 'NONE',  ( 6.125859839683334584, -1.460959015002473382, -0.3926218265389205819 ) ) ;
#36975=CLOSED_SHELL ( 'NONE', ( #66959, #40390, #37437, #50675, #9212, #12312, #64629, #54225, #44860, #65340, #39873, #13303, #2878, #63784, #64293, #8022, #8716, #46404, #40398, #18876, #51054, #46009, #50608, #9878, #18873, #12535, #32545, #47603, #34975, #43922, #67292, #15692, #55990, #3192, #18726, #24225, #39394, #39706, #24356, #17700, #13889 ) ) ;
#37027=DIRECTION ( 'NONE',  ( 1.000000000000000000, 0.000000000000000000, 0.000000000000000000 ) ) ;
#37028=CARTESIAN_POINT ( 'NONE',  ( 6.895370762210000670, -1.248147532381999936, -0.07834881647112000580 ) ) ;
#37125=VERTEX_POINT ( 'NONE', #10694 ) ;
#37126=CARTESIAN_POINT ( 'NONE',  ( 5.003257791993000581, 0.7138878598698999989, -0.8816291593956999684 ) ) ;
#37155=CARTESIAN_POINT ( 'NONE',  ( 6.778816671981999775, -0.8882170986559999593, 0.6661914818925001036 ) ) ;
#37170=ORIENTED_EDGE ( 'NONE', *, *, #30074, .T. ) ;
#37205=CARTESIAN_POINT ( 'NONE',  ( 6.254548602795000356, -0.8406263976572999619, -1.204107458873000081 ) ) ;
#37207=VECTOR ( 'NONE', #7852, 1000.000000000000000 ) ;
#37272=CARTESIAN_POINT ( 'NONE',  ( 0.7000000000000000666, -1.154700538379000108, 0.000000000000000000 ) ) ;
#37280=CARTESIAN_POINT ( 'NONE',  ( 6.894825288116000372, 0.2042423412131999794, -1.256697851460000237 ) ) ;
#37286=DIRECTION ( 'NONE',  ( 0.000000000000000000, -1.000000000000000000, 0.000000000000000000 ) ) ;
#37298=EDGE_LOOP ( 'NONE', ( #43480, #67721, #56333, #56905 ) ) ;
#37303=VERTEX_POINT ( 'NONE', #37272 ) ;
#37334=ORIENTED_EDGE ( 'NONE', *, *, #59255, .T. ) ;
#37339=DIRECTION ( 'NONE',  ( 1.000000000000000000, 0.000000000000000000, 0.000000000000000000 ) ) ;
#37363=CARTESIAN_POINT ( 'NONE',  ( 7.227452085661000503, 0.5737759661892000151, 1.111209200203999936 ) ) ;
#37371=CARTESIAN_POINT ( 'NONE',  ( 6.965816936038000229, -1.147328252452000097, 0.8605332073374000190 ) ) ;
#37437=ADVANCED_FACE ( 'NONE', ( #24979, #41747 ), #4671, .T. ) ;
#37462=CARTESIAN_POINT ( 'NONE',  ( 4.637486820977999358, 1.251140238606999855, -0.2478373488106999922 ) ) ;
#37472=CARTESIAN_POINT ( 'NONE',  ( 4.802943173016458900, 1.199500263597271799, -0.9218200799623701425 ) ) ;
#37497=EDGE_CURVE ( 'NONE', #31811, #65585, #13813, .T. ) ;
#37502=CARTESIAN_POINT ( 'NONE',  ( 7.400000000000000355, 0.000000000000000000, 0.000000000000000000 ) ) ;
#37513=CARTESIAN_POINT ( 'NONE',  ( 5.196297656737999482, 0.2173479397978999861, 1.166870994638999903 ) ) ;
#37537=DIRECTION ( 'NONE',  ( 1.000000000000000000, 0.000000000000000000, -3.330080301313000417E-14 ) ) ;
#37540=CARTESIAN_POINT ( 'NONE',  ( 5.879775144119999908, -0.03703453004475999732, -1.321780775251000017 ) ) ;
#37567=CARTESIAN_POINT ( 'NONE',  ( 6.470987436302001683, 0.1781225934829054336, 1.521768030474604627 ) ) ;
#37581=CARTESIAN_POINT ( 'NONE',  ( 4.990308476675333615, -0.1973919536007287812, 1.504917372998084701 ) ) ;
#37584=CARTESIAN_POINT ( 'NONE',  ( 4.955910294413000017, -1.341011414409000180, 0.4561942916552000349 ) ) ;
#37605=EDGE_CURVE ( 'NONE', #47308, #25728, #10578, .T. ) ;
#37616=CARTESIAN_POINT ( 'NONE',  ( 7.057926398363000509, -1.325960607972999750, 0.7529263492304999472 ) ) ;
#37630=CARTESIAN_POINT ( 'NONE',  ( 5.263359839683333874, 1.310679582531388387, -0.7554284705563470981 ) ) ;
#37648=CARTESIAN_POINT ( 'NONE',  ( 6.188359839683334584, -0.7554284705563480973, -1.310679582531387277 ) ) ;
#37660=ORIENTED_EDGE ( 'NONE', *, *, #67944, .F. ) ;
#37676=CARTESIAN_POINT ( 'NONE',  ( 7.130360733670636719, 1.109723905055048920, -0.6386155440974740083 ) ) ;
#37686=COLOUR_RGB ( '', 0.09019608, 0.27058824, 0.51372549) ;
#37697=AXIS2_PLACEMENT_3D ( 'NONE', #6861, #13508, #39727 ) ;
#37704=AXIS2_PLACEMENT_3D ( 'NONE', #24096, #39141, #8020 ) ;
#37708=CARTESIAN_POINT ( 'NONE',  ( 7.061411423934999654, 0.6837059483940000071, -1.047162964378999916 ) ) ;
#37713=CARTESIAN_POINT ( 'NONE',  ( 6.998282674564999972, -1.401716800305999877, -2.564925509195000141E-10 ) ) ;
#37748=CARTESIAN_POINT ( 'NONE',  ( 5.721693173017332157, 0.7554284705563509839, -1.310679582531386167 ) ) ;
#37763=( NAMED_UNIT ( * ) SI_UNIT ( $, .STERADIAN. ) SOLID_ANGLE_UNIT ( ) );
#37770=FACE_OUTER_BOUND ( 'NONE', #1068, .T. ) ;
#37775=B_SPLINE_CURVE_WITH_KNOTS ( 'NONE', 3,
 ( #2915, #45237, #45914, #9529, #66542, #41361, #13428, #30192, #30872, #52186, #14107, #61307, #9186, #24593, #56057, #61995, #3937, #51498 ),
 .UNSPECIFIED., .F., .F.,
 ( 4, 2, 2, 2, 2, 2, 2, 2, 4 ),
 ( 0.000000000000000000, 0.1250000000000000000, 0.2500000000000000000, 0.3750000000000000000, 0.5000000000000000000, 0.6250000000000000000, 0.7500000000000000000, 0.8750000000000000000, 1.000000000000000000 ),
 .UNSPECIFIED. ) ;
#37808=FACE_OUTER_BOUND ( 'NONE', #36008, .T. ) ;
#37831=CARTESIAN_POINT ( 'NONE',  ( 6.261564796991104132, -0.7389267608984831925, 0.8596156481332365429 ) ) ;
#37842=DIRECTION ( 'NONE',  ( 0.000000000000000000, 0.000000000000000000, 1.000000000000000000 ) ) ;
#37851=B_SPLINE_SURFACE_WITH_KNOTS ( 'NONE', 3, 3, ( 
 ( #67978, #30588, #52250, #31281, #4686, #56818, #51558, #4346, #62396, #68662, #41762, #3998, #20779, #3656, #24994, #47012, #14514, #51899, #25336, #46672, #58872, #143, #27761, #38580, #32315, #6069, #48038, #54311, #26725, #22493, #48733, #27404, #11313, #43136, #16900 ),
 ( #10977, #12012, #835, #22150, #65135, #15873, #6760, #21461, #42795, #43492, #64439, #49071, #53286, #16563, #64103, #42452, #63763, #16217, #37540, #38231, #53628, #5722, #64789, #27065, #59905, #48381, #6412, #59557, #488, #21802, #11657, #37890, #17256, #59210, #32652 ),
 ( #32997, #33348, #47702, #53963, #1183, #43835, #54664, #69013, #21126, #37205, #58523, #10628, #31974, #5386, #2224, #7455, #55358, #14352, #23538, #28806, #38937, #19936, #18303, #40913, #50117, #39279, #66183, #62235, #24836, #14692, #67812, #60948, #1876, #9093, #2555 ),
 ( #36010, #3836, #39627, #34391, #34045, #62572, #1523, #28100, #46510, #44878, #60601, #65488, #35677, #13062, #49413, #55708, #17961, #7806, #29147, #57326, #56991, #49765, #30432, #51743, #12711, #22843, #50454, #46163, #41257, #17614, #44190, #23194, #7114, #67471, #19593 ) ),
 .UNSPECIFIED., .F., .F., .F.,
 ( 4, 4 ),
 ( 4, 1, 1, 1, 1, 1, 1, 1, 1, 1, 1, 1, 1, 1, 1, 1, 1, 1, 1, 1, 1, 1, 1, 1, 1, 1, 1, 1, 1, 1, 1, 1, 4 ),
 ( -0.02636945251836000231, 1.026369452518000047 ),
 ( -0.02000000000000000042, 0.01250000000000000069, 0.04499999999999999833, 0.07749999999999999944, 0.1100000000000000006, 0.1424999999999999878, 0.1749999999999999889, 0.2074999999999999900, 0.2399999999999999911, 0.2725000000000000200, 0.3049999999999999933, 0.3375000000000000222, 0.3699999999999999956, 0.4025000000000000244, 0.4349999999999999978, 0.4675000000000000266, 0.5000000000000000000, 0.5324999999999999734, 0.5649999999999999467, 0.5975000000000000311, 0.6300000000000000044, 0.6624999999999999778, 0.6949999999999999512, 0.7275000000000000355, 0.7600000000000000089, 0.7924999999999999822, 0.8249999999999999556, 0.8575000000000000400, 0.8900000000000000133, 0.9224999999999999867, 0.9549999999999999600, 0.9875000000000000444, 1.020000000000000018 ),
 .UNSPECIFIED. ) ;
#37860=CARTESIAN_POINT ( 'NONE',  ( 4.339059043195999443, 0.6480827609324999461, -1.333028937737999797 ) ) ;
#37864=EDGE_CURVE ( 'NONE', #2054, #95, #29535, .T. ) ;
#37874=CARTESIAN_POINT ( 'NONE',  ( 5.865443173016668510, 1.500000000000000000, 0.1963495408493652339 ) ) ;
#37878=CARTESIAN_POINT ( 'NONE',  ( 4.399712213706658659, 0.7365302470552868019, -1.068880257431492398 ) ) ;
#37890=CARTESIAN_POINT ( 'NONE',  ( 5.224388989100000380, -1.212815126404999999, 0.5269083208682000530 ) ) ;
#37916=CARTESIAN_POINT ( 'NONE',  ( 6.437855742029999107, 0.7705900885230198005, 1.324272068856591211 ) ) ;
#37931=CARTESIAN_POINT ( 'NONE',  ( 4.648022794411000191, 0.6982277932244000951, -1.232437744370999955 ) ) ;
#37948=ORIENTED_EDGE ( 'NONE', *, *, #47837, .T. ) ;
#37981=ORIENTED_EDGE ( 'NONE', *, *, #67347, .F. ) ;
#37982=CARTESIAN_POINT ( 'NONE',  ( 5.477930087360999956, -0.8125565852189000626, 1.395285458375999932 ) ) ;
#38044=ORIENTED_EDGE ( 'NONE', *, *, #59112, .T. ) ;
#38046=CARTESIAN_POINT ( 'NONE',  ( 7.227324660199999862, 1.322954291153000117, 0.3512839726887999614 ) ) ;
#38083=B_SPLINE_CURVE_WITH_KNOTS ( 'NONE', 3,
 ( #6499, #7200, #51479, #59643, #46242, #14086, #49848, #45563, #44276, #3576 ),
 .UNSPECIFIED., .F., .F.,
 ( 4, 2, 2, 2, 4 ),
 ( 0.000000000000000000, 0.1250000005483845322, 0.2500000010967690645, 0.3750000016451535134, 0.5000000021935380179 ),
 .UNSPECIFIED. ) ;
#38103=( NAMED_UNIT ( * ) PLANE_ANGLE_UNIT ( ) SI_UNIT ( $, .RADIAN. ) );
#38159=ORIENTED_EDGE ( 'NONE', *, *, #53598, .T. ) ;
#38167=CARTESIAN_POINT ( 'NONE',  ( 6.455467915152659941, 0.005977207969617732465, -1.133219647842097499 ) ) ;
#38199=CARTESIAN_POINT ( 'NONE',  ( 4.249401635788000675, -0.8829617685141000205, -1.096690919835000111 ) ) ;
#38209=CARTESIAN_POINT ( 'NONE',  ( 4.503351004233334010, -1.211624111678819782, 0.9172058655087356183 ) ) ;
#38226=DIRECTION ( 'NONE',  ( 0.000000000000000000, -0.5000000000000169864, 0.8660254037844288266 ) ) ;
#38231=CARTESIAN_POINT ( 'NONE',  ( 5.829360824503000416, -0.8123280412348000690, -1.043359539020999982 ) ) ;
#38269=CARTESIAN_POINT ( 'NONE',  ( 6.252943173016667799, 1.199500263597271577, -0.9218200799623702535 ) ) ;
#38274=CARTESIAN_POINT ( 'NONE',  ( 4.453300434508999928, -0.3367241447620000216, 1.520685311087999869 ) ) ;
#38326=CARTESIAN_POINT ( 'NONE',  ( 6.385387840465999609, 0.9584732047324999726, 1.299486219972000089 ) ) ;
#38394=CARTESIAN_POINT ( 'NONE',  ( 7.094619556280000516, 1.049447144279999966, -0.6801946707396000491 ) ) ;
#38426=B_SPLINE_SURFACE_WITH_KNOTS ( 'NONE', 3, 3, ( 
 ( #64198, #53724, #11753, #28193, #65238, #33790, #17353, #55106, #54412, #60002, #11408, #43235, #7212, #1621, #38326, #49508, #1276, #12113, #16999, #49163, #27501, #22246, #240, #12457, #22936, #44288, #33441, #58970, #16656, #588, #21897, #64539, #37982, #65586, #27160 ),
 ( #38681, #48136, #54757, #21555, #6512, #6856, #32747, #59306, #42891, #17711, #59656, #39034, #22591, #60349, #33095, #43933, #48827, #43584, #16313, #11074, #32409, #5821, #48481, #54063, #6160, #936, #64885, #27857, #18397, #51237, #7549, #18055, #45657, #39372, #44635 ),
 ( #65927, #40397, #60691, #28903, #2651, #39723, #67300, #13162, #7903, #3334, #66275, #34490, #50895, #34825, #35508, #14180, #18743, #61720, #62066, #66964, #13839, #56137, #12808, #34137, #55801, #44971, #45988, #24667, #23979, #8245, #50551, #55454, #24324, #29241, #19417 ),
 ( #45314, #66621, #29933, #28549, #56828, #61385, #40074, #61041, #35169, #40741, #13505, #50210, #2990, #19070, #2311, #23633, #29592, #56481, #8585, #49859, #1972, #23294, #4008, #15202, #26388, #4697, #26040, #47369, #41773, #46685, #51912, #42464, #4358, #47023, #20105 ) ),
 .UNSPECIFIED., .F., .F., .F.,
 ( 4, 4 ),
 ( 4, 1, 1, 1, 1, 1, 1, 1, 1, 1, 1, 1, 1, 1, 1, 1, 1, 1, 1, 1, 1, 1, 1, 1, 1, 1, 1, 1, 1, 1, 1, 1, 4 ),
 ( -0.02636945251836000231, 1.026369452518000047 ),
 ( -0.02000000000000000042, 0.01250000000000000069, 0.04499999999999999833, 0.07749999999999999944, 0.1100000000000000006, 0.1424999999999999878, 0.1749999999999999889, 0.2074999999999999900, 0.2399999999999999911, 0.2725000000000000200, 0.3049999999999999933, 0.3375000000000000222, 0.3699999999999999956, 0.4025000000000000244, 0.4349999999999999978, 0.4675000000000000266, 0.5000000000000000000, 0.5324999999999999734, 0.5649999999999999467, 0.5975000000000000311, 0.6300000000000000044, 0.6624999999999999778, 0.6949999999999999512, 0.7275000000000000355, 0.7600000000000000089, 0.7924999999999999822, 0.8249999999999999556, 0.8575000000000000400, 0.8900000000000000133, 0.9224999999999999867, 0.9549999999999999600, 0.9875000000000000444, 1.020000000000000018 ),
 .UNSPECIFIED. ) ;
#38439=CARTESIAN_POINT ( 'NONE',  ( 5.607109839683542596, -1.199500263597270244, -0.9218200799623728070 ) ) ;
#38440=ORIENTED_EDGE ( 'NONE', *, *, #21523, .F. ) ;
#38455=( NAMED_UNIT ( * ) SI_UNIT ( $, .STERADIAN. ) SOLID_ANGLE_UNIT ( ) );
#38497=DIRECTION ( 'NONE',  ( -1.000000000000000000, 0.000000000000000000, 0.000000000000000000 ) ) ;
#38522=CARTESIAN_POINT ( 'NONE',  ( 5.453635137985188841, -0.01427739589657720659, -1.132912223412962271 ) ) ;
#38550=CARTESIAN_POINT ( 'NONE',  ( 5.250092101183000182, -0.5193948854954000272, 0.9696677542920000281 ) ) ;
#38580=CARTESIAN_POINT ( 'NONE',  ( 5.706658963913000093, 0.06352927768877000836, 1.174369886990999978 ) ) ;
#38624=CARTESIAN_POINT ( 'NONE',  ( 4.613813072189000053, 0.1210501919378999952, -1.411301419693000048 ) ) ;
#38681=CARTESIAN_POINT ( 'NONE',  ( 6.961818577609000691, -1.329569516000000062, 0.3446834961110000206 ) ) ;
#38760=VECTOR ( 'NONE', #6533, 1000.000000000000000 ) ;
#38789=CARTESIAN_POINT ( 'NONE',  ( 5.575859839683415586, -1.460959015002473826, -0.3926218265389207485 ) ) ;
#38878=CARTESIAN_POINT ( 'NONE',  ( 6.277723390171241924, -0.9000774111393842203, 0.6873532864722641245 ) ) ;
#38907=CARTESIAN_POINT ( 'NONE',  ( 5.074249783945999681, -0.3757116368264999950, 1.356905753638999901 ) ) ;
#38937=CARTESIAN_POINT ( 'NONE',  ( 5.699991087009000701, -1.413039514337999902, -0.3998085520867999954 ) ) ;
#39034=CARTESIAN_POINT ( 'NONE',  ( 6.457675381438999551, -1.400415568386000009, 0.4419997549869000286 ) ) ;
#39064=CARTESIAN_POINT ( 'NONE',  ( 5.940443173017124323, -0.1963495408493673156, 1.499999999999999556 ) ) ;
#39066=EDGE_LOOP ( 'NONE', ( #22698, #45816, #16499, #54165 ) ) ;
#39103=ORIENTED_EDGE ( 'NONE', *, *, #7617, .T. ) ;
#39123=VERTEX_POINT ( 'NONE', #59571 ) ;
#39141=DIRECTION ( 'NONE',  ( 1.000000000000000000, 0.000000000000000000, 0.000000000000000000 ) ) ;
#39208=CARTESIAN_POINT ( 'NONE',  ( 4.605026506348999682, -1.500000000000000000, 0.000000000000000000 ) ) ;
#39218=CARTESIAN_POINT ( 'NONE',  ( 6.003027306108891459, 0.6725737735649598426, -0.9715352586480965336 ) ) ;
#39248=CARTESIAN_POINT ( 'NONE',  ( 4.529075847544000055, -1.038563345233000090, 1.255970712535000144 ) ) ;
#39279=CARTESIAN_POINT ( 'NONE',  ( 5.447919488923999687, 1.422967556274000067, 0.3628923349178999613 ) ) ;
#39296=ORIENTED_EDGE ( 'NONE', *, *, #29958, .T. ) ;
#39372=CARTESIAN_POINT ( 'NONE',  ( 5.365365123072000308, -0.1429527940584000290, 1.396516134632999950 ) ) ;
#39394=ADVANCED_FACE ( 'NONE', ( #5318 ), #64981, .T. ) ;
#39406=CARTESIAN_POINT ( 'NONE',  ( 1.700000000000000178, 0.000000000000000000, 0.000000000000000000 ) ) ;
#39500=EDGE_CURVE ( 'NONE', #14587, #9931, #61649, .T. ) ;
#39522=CARTESIAN_POINT ( 'NONE',  ( 5.403413393859333169, 0.4964519701263342411, 1.434320509598691507 ) ) ;
#39559=VERTEX_POINT ( 'NONE', #13259 ) ;
#39623=APPLICATION_CONTEXT ( 'automotive_design' ) ;
#39627=CARTESIAN_POINT ( 'NONE',  ( 6.528493422235999155, -1.019889730527999916, 1.251756626546000062 ) ) ;
#39635=FACE_OUTER_BOUND ( 'NONE', #45745, .T. ) ;
#39654=CARTESIAN_POINT ( 'NONE',  ( 4.825859839683332986, 1.460959015002472494, 0.3926218265389232465 ) ) ;
#39667=LINE ( 'NONE', #30468, #37207 ) ;
#39706=ADVANCED_FACE ( 'NONE', ( #49876 ), #50910, .T. ) ;
#39714=CYLINDRICAL_SURFACE ( 'NONE', #56623, 1.500000000000000000 ) ;
#39723=CARTESIAN_POINT ( 'NONE',  ( 6.681205881262999746, 1.240385862733000000, 0.4581726639353000397 ) ) ;
#39727=DIRECTION ( 'NONE',  ( 0.000000000000000000, 0.000000000000000000, 1.000000000000000000 ) ) ;
#39741=CARTESIAN_POINT ( 'NONE',  ( 0.2000000000000000389, 0.000000000000000000, 0.000000000000000000 ) ) ;
#39817=ORIENTED_EDGE ( 'NONE', *, *, #64503, .T. ) ;
#39873=ADVANCED_FACE ( 'NONE', ( #34069 ), #12740, .F. ) ;
#40074=CARTESIAN_POINT ( 'NONE',  ( 6.551836143767999943, 1.130384497037000058, -0.3246714051208999807 ) ) ;
#40108=EDGE_CURVE ( 'NONE', #3750, #66643, #46974, .T. ) ;
#40265=EDGE_CURVE ( 'NONE', #11589, #39123, #23722, .T. ) ;
#40313=CARTESIAN_POINT ( 'NONE',  ( 0.7000000000000000666, 0.5773502691895999739, 1.000000000000000000 ) ) ;
#40345=CARTESIAN_POINT ( 'NONE',  ( 0.000000000000000000, 0.000000000000000000, 0.000000000000000000 ) ) ;
#40375=CARTESIAN_POINT ( 'NONE',  ( 4.555026506349999948, -1.500000000000000000, 0.000000000000000000 ) ) ;
#40390=ADVANCED_FACE ( 'NONE', ( #66739 ), #59066, .F. ) ;
#40397=CARTESIAN_POINT ( 'NONE',  ( 6.866058386525000223, -1.131649478240000173, 0.5631818380099999910 ) ) ;
#40398=ADVANCED_FACE ( 'NONE', ( #37808 ), #53858, .T. ) ;
#40516=VERTEX_POINT ( 'NONE', #12284 ) ;
#40518=ORIENTED_EDGE ( 'NONE', *, *, #33055, .F. ) ;
#40551=ORIENTED_EDGE ( 'NONE', *, *, #67944, .T. ) ;
#40631=LINE ( 'NONE', #62305, #66528 ) ;
#40685=VERTEX_POINT ( 'NONE', #12431 ) ;
#40716=ORIENTED_EDGE ( 'NONE', *, *, #21080, .F. ) ;
#40741=CARTESIAN_POINT ( 'NONE',  ( 6.400593184916999689, -0.6732323296109999911, -0.9643333493903999409 ) ) ;
#40789=EDGE_CURVE ( 'NONE', #36346, #68681, #22562, .T. ) ;
#40878=VERTEX_POINT ( 'NONE', #59629 ) ;
#40883=CARTESIAN_POINT ( 'NONE',  ( 7.267555237352232744, -0.6773954909162061000, 0.9416021803066277895 ) ) ;
#40892=CARTESIAN_POINT ( 'NONE',  ( 7.193989102394000135, 0.8129426006129999438, -1.245101619383000235 ) ) ;
#40913=CARTESIAN_POINT ( 'NONE',  ( 5.548748128158000448, 0.07932534654105999339, 1.466367974616999748 ) ) ;
#41036=DIRECTION ( 'NONE',  ( 1.000000000000000000, 0.000000000000000000, -9.843114642662001530E-13 ) ) ;
#41076=LINE ( 'NONE', #30934, #32226 ) ;
#41114=CARTESIAN_POINT ( 'NONE',  ( 5.469609839683874597, 0.1963495408493571015, 1.500000000000000444 ) ) ;
#41122=CARTESIAN_POINT ( 'NONE',  ( 5.282109839684041575, 0.9218200799623742503, -1.199500263597268912 ) ) ;
#41257=CARTESIAN_POINT ( 'NONE',  ( 5.217721112195000899, -0.1291622704458000037, -1.609550399409999999 ) ) ;
#41270=EDGE_CURVE ( 'NONE', #2358, #40685, #27647, .T. ) ;
#41340=CARTESIAN_POINT ( 'NONE',  ( 4.466438209866000264, -0.8917438941569999500, -0.9119035439078000405 ) ) ;
#41361=CARTESIAN_POINT ( 'NONE',  ( 6.799634134627482673, 1.520134557123164365, -0.1051316465493104674 ) ) ;
#41465=CARTESIAN_POINT ( 'NONE',  ( 5.115443173016708478, -1.500000000000000222, -0.1963495408493622085 ) ) ;
#41491=CARTESIAN_POINT ( 'NONE',  ( 7.006988838338999770, 0.6190876222846001253, -0.9481936368762999834 ) ) ;
#41499=VERTEX_POINT ( 'NONE', #35577 ) ;
#41530=ORIENTED_EDGE ( 'NONE', *, *, #31763, .F. ) ;
#41540=DIRECTION ( 'NONE',  ( 1.000000000000000000, 0.000000000000000000, 0.000000000000000000 ) ) ;
#41554=FACE_OUTER_BOUND ( 'NONE', #60072, .T. ) ;
#41606=DIRECTION ( 'NONE',  ( -1.000000000000000000, 0.000000000000000000, 0.000000000000000000 ) ) ;
#41607=ORIENTED_EDGE ( 'NONE', *, *, #61029, .T. ) ;
#41621=CARTESIAN_POINT ( 'NONE',  ( 1.700000000000000178, -2.149999999999999911, 0.000000000000000000 ) ) ;
#41679=CARTESIAN_POINT ( 'NONE',  ( 4.729580014212999117, -0.4240496150661999808, 1.052182387563999955 ) ) ;
#41707=AXIS2_PLACEMENT_3D ( 'NONE', #68448, #41895, #14982 ) ;
#41747=FACE_OUTER_BOUND ( 'NONE', #97, .T. ) ;
#41749=CARTESIAN_POINT ( 'NONE',  ( 4.752943173016667799, 1.199500263597271577, -0.9218200799623702535 ) ) ;
#41752=AXIS2_PLACEMENT_3D ( 'NONE', #8379, #51025, #18870 ) ;
#41762=CARTESIAN_POINT ( 'NONE',  ( 6.362045118933999710, -1.113463867511000238, -0.3786539577593999728 ) ) ;
#41773=CARTESIAN_POINT ( 'NONE',  ( 5.442721112194999655, -0.09407552946282000950, -1.172318398388999983 ) ) ;
#41804=CARTESIAN_POINT ( 'NONE',  ( 5.171704601181000172, -0.2775142444059999769, -1.532592734373000143 ) ) ;
#41834=CARTESIAN_POINT ( 'NONE',  ( 6.840948176613999898, -1.130182777988000042, -0.07094392349790000496 ) ) ;
#41895=DIRECTION ( 'NONE',  ( 0.000000000000000000, -0.8660254037844288266, -0.5000000000000169864 ) ) ;
#41951=CARTESIAN_POINT ( 'NONE',  ( 5.625859839683333696, -1.460959015002473382, -0.3926218265389205819 ) ) ;
#42008=CARTESIAN_POINT ( 'NONE',  ( 4.652221739856806870, 0.7358276262617508001, 0.9460093964854561222 ) ) ;
#42029=CARTESIAN_POINT ( 'NONE',  ( 5.140096680883000424, 0.7660746065864000309, 0.8366799443169999906 ) ) ;
#42076=DIRECTION ( 'NONE',  ( 0.000000000000000000, 0.000000000000000000, 1.000000000000000000 ) ) ;
#42095=CARTESIAN_POINT ( 'NONE',  ( 4.399671512406701623, 1.282007644070062957, -0.5110265287773028131 ) ) ;
#42130=ORIENTED_EDGE ( 'NONE', *, *, #20431, .F. ) ;
#42169=CARTESIAN_POINT ( 'NONE',  ( 4.468342168782999835, 0.2293269131957661466, 1.516947103425834831 ) ) ;
#42191=CARTESIAN_POINT ( 'NONE',  ( 7.160490346876999368, -0.4460864650370000017, 1.192484047995999941 ) ) ;
#42247=CARTESIAN_POINT ( 'NONE',  ( 7.077542425583873253, -1.465994342824544899E-06, -1.322443989608400816 ) ) ;
#42255=PLANE ( 'NONE',  #41707 ) ;
#42269=CARTESIAN_POINT ( 'NONE',  ( 7.201087902152560005, 0.7854182645431827536, 0.9439803561485179406 ) ) ;
#42279=CARTESIAN_POINT ( 'NONE',  ( 7.127955114086000243, 0.8827681146003000245, 0.7092679259177999684 ) ) ;
#42282=APPLICATION_CONTEXT ( 'automotive_design' ) ;
#42309=CARTESIAN_POINT ( 'NONE',  ( 5.740443173016667622, 0.1963495408493638184, -1.499999999999999778 ) ) ;
#42357=CARTESIAN_POINT ( 'NONE',  ( 4.813605073191808970, -1.173669780889472936, 0.2426414077541297898 ) ) ;
#42377=CARTESIAN_POINT ( 'NONE',  ( 4.705906265422999724, 1.004282239496999907, 0.7862521424935998704 ) ) ;
#42437=CARTESIAN_POINT ( 'NONE',  ( 4.627943173016668688, -0.9218200799623714747, -1.199500263597270466 ) ) ;
#42452=CARTESIAN_POINT ( 'NONE',  ( 6.031018102971001049, 1.262548346495000029, 0.3929982786279000440 ) ) ;
#42464=CARTESIAN_POINT ( 'NONE',  ( 5.291478153344000290, -1.078708783361999934, 0.4686457328678000356 ) ) ;
#42479=DIRECTION ( 'NONE',  ( 1.000000000000000000, 0.000000000000000000, 0.000000000000000000 ) ) ;
#42490=CARTESIAN_POINT ( 'NONE',  ( 6.138359839683334762, -0.7554284705563483193, -1.310679582531387721 ) ) ;
#42527=CARTESIAN_POINT ( 'NONE',  ( 6.874156308958999873, -1.004440062237000220, -0.5229138879281000074 ) ) ;
#42554=CARTESIAN_POINT ( 'NONE',  ( 6.302943173016666734, 1.199500263597271799, -0.9218200799623701425 ) ) ;
#42612=CARTESIAN_POINT ( 'NONE',  ( 6.773735035739000487, -0.8949653936606000171, 0.6576296519798999762 ) ) ;
#42641=CARTESIAN_POINT ( 'NONE',  ( 5.657109839683332808, -1.199500263597270022, -0.9218200799623730290 ) ) ;
#42674=DIRECTION ( 'NONE',  ( -1.000000000000000000, 0.000000000000000000, 0.000000000000000000 ) ) ;
#42678=ORIENTED_EDGE ( 'NONE', *, *, #9605, .T. ) ;
#42689=CARTESIAN_POINT ( 'NONE',  ( 4.706016184301807570, -0.01789162623760187643, 1.198355196476257545 ) ) ;
#42702=VERTEX_POINT ( 'NONE', #56476 ) ;
#42714=CARTESIAN_POINT ( 'NONE',  ( 4.934838347548000215, -0.2021279076763000115, -1.116266169982000234 ) ) ;
#42762=CARTESIAN_POINT ( 'NONE',  ( 4.765942101178999302, -0.7564391385043001126, 0.9147881139243999593 ) ) ;
#42795=CARTESIAN_POINT ( 'NONE',  ( 6.383918340290000160, 0.03180299129942999736, -1.321917036380999999 ) ) ;
#42836=CARTESIAN_POINT ( 'NONE',  ( 4.819071405523000173, 0.6499247483229999567, 1.258579622759999905 ) ) ;
#42871=CARTESIAN_POINT ( 'NONE',  ( 6.940572573649000709, -0.2869491282519000541, -1.095445449434000018 ) ) ;
#42891=CARTESIAN_POINT ( 'NONE',  ( 6.608918340290000693, 0.03531958898060999497, -1.468087261088999895 ) ) ;
#42898=CARTESIAN_POINT ( 'NONE',  ( 6.209193173016666734, -0.3926218265389190276, -1.460959015002473826 ) ) ;
#42947=EDGE_CURVE ( 'NONE', #58024, #426, #34276, .T. ) ;
#42954=DIRECTION ( 'NONE',  ( 0.000000000000000000, -1.000000000000000000, 0.000000000000000000 ) ) ;
#42955=CARTESIAN_POINT ( 'NONE',  ( 7.161035820969999577, 1.208716259960000095, 0.3209503551946999989 ) ) ;
#42967=ORIENTED_EDGE ( 'NONE', *, *, #8134, .T. ) ;
#43076=CARTESIAN_POINT ( 'NONE',  ( 6.326199169711658854, -1.131438764395593655, 0.04874608710810101470 ) ) ;
#43078=CONICAL_SURFACE ( 'NONE', #31914, 1.200857723089999940, 0.7853979760808852406 ) ;
#43079=CARTESIAN_POINT ( 'NONE',  ( 1.700000000000000178, -1.500000000000000000, 0.000000000000000000 ) ) ;
#43082=CARTESIAN_POINT ( 'NONE',  ( 6.868195110880497722, -1.013868087716280009, -0.5278221404403410366 ) ) ;
#43108=CARTESIAN_POINT ( 'NONE',  ( 5.063547794415999448, 1.011671888745000025, 0.8705125097731000183 ) ) ;
#43117=CARTESIAN_POINT ( 'NONE',  ( 6.000859839683335473, -0.3926218265389255779, 1.460959015002472494 ) ) ;
#43122=CARTESIAN_POINT ( 'NONE',  ( 4.399769195526705978, -0.2610650747889547429, -1.154523729464906001 ) ) ;
#43129=CARTESIAN_POINT ( 'NONE',  ( 4.605026506348999682, -1.500000000000000000, 0.000000000000000000 ) ) ;
#43136=CARTESIAN_POINT ( 'NONE',  ( 5.219320540948999998, -0.1144865814785000074, 1.118427654993999987 ) ) ;
#43174=CARTESIAN_POINT ( 'NONE',  ( 6.294609839683335650, 1.500000000000001110, -0.1963495408493590721 ) ) ;
#43177=CARTESIAN_POINT ( 'NONE',  ( 6.553816671982000130, -1.199981415667000118, 0.9000247785775999931 ) ) ;
#43179=CARTESIAN_POINT ( 'NONE',  ( 4.317328812926999326, 0.6646734451123000875, 1.217994223230000062 ) ) ;
#43235=CARTESIAN_POINT ( 'NONE',  ( 6.536630799317000751, -1.539848055637000002, 0.4860074956841999860 ) ) ;
#43285=B_SPLINE_CURVE_WITH_KNOTS ( 'NONE', 3,
 ( #37371, #69178, #48554, #37713 ),
 .UNSPECIFIED., .F., .F.,
 ( 4, 4 ),
 ( 0.000000000000000000, 1.000000000000000000 ),
 .UNSPECIFIED. ) ;
#43287=CONICAL_SURFACE ( 'NONE', #60055, 1.249999322936999890, 0.7853979760808852406 ) ;
#43303=CARTESIAN_POINT ( 'NONE',  ( 7.349215237593000438, -1.066568762865999886, 0.6056346772294000091 ) ) ;
#43362=AXIS2_PLACEMENT_3D ( 'NONE', #46427, #35257, #67053 ) ;
#43422=CARTESIAN_POINT ( 'NONE',  ( 4.657109839682542329, -1.199500263597270022, -0.9218200799623730290 ) ) ;
#43435=CARTESIAN_POINT ( 'NONE',  ( 5.744489815226755169, -0.5444585885964672300, 0.9942383223988339180 ) ) ;
#43464=FACE_OUTER_BOUND ( 'NONE', #46112, .T. ) ;
#43474=CARTESIAN_POINT ( 'NONE',  ( 6.105026506350000659, -1.500000000000000000, 0.000000000000000000 ) ) ;
#43480=ORIENTED_EDGE ( 'NONE', *, *, #12236, .T. ) ;
#43492=CARTESIAN_POINT ( 'NONE',  ( 6.333504020672999779, -0.7569293636342000475, -1.084220404132000048 ) ) ;
#43532=CARTESIAN_POINT ( 'NONE',  ( 5.161168627748000226, 0.8913906144712999691, -1.100839504782000100 ) ) ;
#43540=CARTESIAN_POINT ( 'NONE',  ( 4.605026506348999682, -1.500000000000000000, 0.000000000000000000 ) ) ;
#43584=CARTESIAN_POINT ( 'NONE',  ( 6.155189463736999933, 0.8358542970315000487, -1.207425004536999857 ) ) ;
#43608=B_SPLINE_CURVE_WITH_KNOTS ( 'NONE', 3,
 ( #30342, #35244, #30677, #51648, #31030, #13579, #56215, #67715, #19841, #8325, #50971, #3067, #45730, #48130, #37630, #63850, #26814, #5128 ),
 .UNSPECIFIED., .F., .F.,
 ( 4, 2, 2, 2, 2, 2, 2, 2, 4 ),
 ( 0.000000000000000000, 0.1250000000000000000, 0.2500000000000000000, 0.3750000000000000000, 0.5000000000000000000, 0.6250000000000000000, 0.7500000000000000000, 0.8750000000000000000, 1.000000000000000000 ),
 .UNSPECIFIED. ) ;
#43612=AXIS2_PLACEMENT_3D ( 'NONE', #4850, #30750, #36684 ) ;
#43624=CARTESIAN_POINT ( 'NONE',  ( 5.971693173017000866, -0.7554284705563540925, 1.310679582531384391 ) ) ;
#43651=CARTESIAN_POINT ( 'NONE',  ( 7.127827688624999602, 1.235070164474999954, -0.1964835531513000055 ) ) ;
#43655=DIRECTION ( 'NONE',  ( 0.000000000000000000, 0.5000000000000169864, 0.8660254037844288266 ) ) ;
#43777=CARTESIAN_POINT ( 'NONE',  ( 5.647538256146063418, 0.7451564378516357667, 0.8540504721569680546 ) ) ;
#43790=EDGE_LOOP ( 'NONE', ( #20393, #32189 ) ) ;
#43806=CARTESIAN_POINT ( 'NONE',  ( 4.525603349966000444, 1.298316671829000013, 0.3090933427313000137 ) ) ;
#43815=CARTESIAN_POINT ( 'NONE',  ( 4.400000000000000355, 0.5526513453421999511, 1.394480724316999876 ) ) ;
#43835=CARTESIAN_POINT ( 'NONE',  ( 6.456205881263000101, 1.377540824270000019, 0.5088348457508999889 ) ) ;
#43859=CARTESIAN_POINT ( 'NONE',  ( 6.537250824846000619, -1.012620940260093416, 1.149827999411389357 ) ) ;
#43874=CARTESIAN_POINT ( 'NONE',  ( 4.419090712286999789, 0.3277123218568999685, 1.522640465285999944 ) ) ;
#43879=EDGE_CURVE ( 'NONE', #59129, #68689, #36502, .T. ) ;
#43904=CARTESIAN_POINT ( 'NONE',  ( -0.2999999999999999889, 0.5773502691895999739, 1.000000000000000000 ) ) ;
#43913=CARTESIAN_POINT ( 'NONE',  ( 6.637290055325000715, -1.379059567415999998, -0.7179416942773999555 ) ) ;
#43922=ADVANCED_FACE ( 'NONE', ( #8236 ), #39714, .T. ) ;
#43933=CARTESIAN_POINT ( 'NONE',  ( 6.256018102970999806, 1.402153912072999997, 0.4364538398439999911 ) ) ;
#43962=DIRECTION ( 'NONE',  ( 1.000000000000000000, 0.000000000000000000, 0.000000000000000000 ) ) ;
#44039=ORIENTED_EDGE ( 'NONE', *, *, #9007, .T. ) ;
#44096=CARTESIAN_POINT ( 'NONE',  ( 6.778816671981999775, -0.8882170986559999593, 0.6661914818925001036 ) ) ;
#44131=CARTESIAN_POINT ( 'NONE',  ( 6.116137458369862223, 1.019062767528970737, 0.4963261465187597254 ) ) ;
#44160=CARTESIAN_POINT ( 'NONE',  ( 5.117342238861000148, 0.2443688909792999520, 1.311937767346999850 ) ) ;
#44190=CARTESIAN_POINT ( 'NONE',  ( 5.116892472961001026, -1.574491786429000006, -0.3581626104627999574 ) ) ;
#44211=VECTOR ( 'NONE', #38226, 1000.000000000000114 ) ;
#44271=VERTEX_POINT ( 'NONE', #11658 ) ;
#44276=CARTESIAN_POINT ( 'NONE',  ( 7.070925607327942508, -0.1731109087963655924, -1.329073895981641495 ) ) ;
#44288=CARTESIAN_POINT ( 'NONE',  ( 5.830830324679999954, 1.564645433990000001, 0.3990237390554000063 ) ) ;
#44299=EDGE_LOOP ( 'NONE', ( #24163, #14697, #23787, #61493, #33058 ) ) ;
#44368=DIRECTION ( 'NONE',  ( 1.000000000000000000, 0.000000000000000000, 0.000000000000000000 ) ) ;
#44426=DIRECTION ( 'NONE',  ( 1.000000000000000000, 0.000000000000000000, 0.000000000000000000 ) ) ;
#44455=ORIENTED_EDGE ( 'NONE', *, *, #37605, .T. ) ;
#44456=DIRECTION ( 'NONE',  ( 1.000000000000000000, 0.000000000000000000, 0.000000000000000000 ) ) ;
#44467=CARTESIAN_POINT ( 'NONE',  ( 5.855026506350000659, 1.500000000000000000, 0.000000000000000000 ) ) ;
#44484=CARTESIAN_POINT ( 'NONE',  ( 6.083820272009583974, 1.131309771130457609, 0.05987387093659040510 ) ) ;
#44492=CARTESIAN_POINT ( 'NONE',  ( 5.537956561560666735, -1.500000000000001332, 0.3217608788839214085 ) ) ;
#44510=CARTESIAN_POINT ( 'NONE',  ( 4.152514736428999598, -1.182555397712999889, -0.9394135237491000323 ) ) ;
#44600=ORIENTED_EDGE ( 'NONE', *, *, #5648, .T. ) ;
#44635=CARTESIAN_POINT ( 'NONE',  ( 5.348560349866000152, 0.1454693244516999939, 1.365796648849999961 ) ) ;
#44642=ORIENTED_EDGE ( 'NONE', *, *, #9736, .F. ) ;
#44666=CARTESIAN_POINT ( 'NONE',  ( 5.805026506351000037, 1.500000000000000000, 0.000000000000000000 ) ) ;
#44676=CARTESIAN_POINT ( 'NONE',  ( 6.813937712952314207, 1.320991801770956098, -0.7472670741277307460 ) ) ;
#44723=VERTEX_POINT ( 'NONE', #44467 ) ;
#44730=CARTESIAN_POINT ( 'NONE',  ( 1.700000000000000178, 0.000000000000000000, 0.000000000000000000 ) ) ;
#44769=CYLINDRICAL_SURFACE ( 'NONE', #49922, 1.000000000000000000 ) ;
#44844=VERTEX_POINT ( 'NONE', #50898 ) ;
#44860=ADVANCED_FACE ( 'NONE', ( #23636 ), #13165, .F. ) ;
#44878=CARTESIAN_POINT ( 'NONE',  ( 6.175593184917000045, -0.9243234316805000184, -1.323994513613999890 ) ) ;
#44887=DIRECTION ( 'NONE',  ( 1.000000000000000000, 0.000000000000000000, 0.000000000000000000 ) ) ;
#44915=ORIENTED_EDGE ( 'NONE', *, *, #67347, .T. ) ;
#44919=FACE_OUTER_BOUND ( 'NONE', #59736, .T. ) ;
#44971=CARTESIAN_POINT ( 'NONE',  ( 5.672919488924000220, 1.281289678559000000, 0.3267609307802000207 ) ) ;
#45014=CARTESIAN_POINT ( 'NONE',  ( 6.875386523732225363, 1.468717224916136654, 0.3829316497910061345 ) ) ;
#45057=ORIENTED_EDGE ( 'NONE', *, *, #46095, .F. ) ;
#45118=CARTESIAN_POINT ( 'NONE',  ( 5.452606837613999780, -0.4199405305951999789, 1.440017343911000003 ) ) ;
#45237=CARTESIAN_POINT ( 'NONE',  ( 6.885860368544080679, 0.8047703218898319966, 1.294940731405771706 ) ) ;
#45284=DIRECTION ( 'NONE',  ( 1.000000000000000000, 0.000000000000000000, 0.000000000000000000 ) ) ;
#45305=CARTESIAN_POINT ( 'NONE',  ( 1.700000000000000178, 0.000000000000000000, 0.000000000000000000 ) ) ;
#45314=CARTESIAN_POINT ( 'NONE',  ( 6.803907741853000957, -1.064812127159999955, 0.2760466167989999997 ) ) ;
#45336=CARTESIAN_POINT ( 'NONE',  ( 5.605026506349999771, -1.500000000000000000, 0.000000000000000000 ) ) ;
#45430=CARTESIAN_POINT ( 'NONE',  ( 5.468188860442999122, -0.6025205152629000693, 1.401692221310999908 ) ) ;
#45499=ORIENTED_EDGE ( 'NONE', *, *, #11200, .F. ) ;
#45556=DIRECTION ( 'NONE',  ( 0.000000000000000000, -1.000000000000000000, 0.000000000000000000 ) ) ;
#45563=CARTESIAN_POINT ( 'NONE',  ( 7.064321704349473485, -0.3488121830932555678, -1.301244489718812236 ) ) ;
#45567=PRODUCT_DEFINITION_SHAPE ( 'NONE', 'NONE',  #2199 ) ;
#45657=CARTESIAN_POINT ( 'NONE',  ( 5.398974669483000532, -0.7389799844016000652, 1.268943043503000023 ) ) ;
#45730=CARTESIAN_POINT ( 'NONE',  ( 5.232109839683333874, 0.9218200799623741393, -1.199500263597268690 ) ) ;
#45745=EDGE_LOOP ( 'NONE', ( #3856, #28991, #10416 ) ) ;
#45765=CARTESIAN_POINT ( 'NONE',  ( 6.502943173016666911, -1.199500263597274241, 0.9218200799623669228 ) ) ;
#45813=DIRECTION ( 'NONE',  ( 1.000000000000000000, 0.000000000000000000, 9.841108777351999576E-13 ) ) ;
#45816=ORIENTED_EDGE ( 'NONE', *, *, #13106, .T. ) ;
#45853=CARTESIAN_POINT ( 'NONE',  ( 7.257235050943683596, -0.9062970480449128452, 0.7219501443736217050 ) ) ;
#45914=CARTESIAN_POINT ( 'NONE',  ( 6.871489329557980419, 1.027917644197982705, 1.125047304260232917 ) ) ;
#45928=CARTESIAN_POINT ( 'NONE',  ( 4.919609839683332986, 0.1963495408493571848, 1.500000000000000666 ) ) ;
#45977=AXIS2_PLACEMENT_3D ( 'NONE', #51255, #13521, #3008 ) ;
#45988=CARTESIAN_POINT ( 'NONE',  ( 5.622505169306999839, 1.226089021931999978, -0.4951583500558000006 ) ) ;
#45989=SHAPE_DEFINITION_REPRESENTATION ( #45567, #26842 ) ;
#46009=ADVANCED_FACE ( 'NONE', ( #57583 ), #38426, .F. ) ;
#46095=EDGE_CURVE ( 'NONE', #37303, #40878, #14525, .T. ) ;
#46112=EDGE_LOOP ( 'NONE', ( #5725, #18009, #22986, #15484, #28108, #44455 ) ) ;
#46163=CARTESIAN_POINT ( 'NONE',  ( 5.268135431812000391, 0.8487381973356000753, -1.373673328256999948 ) ) ;
#46242=CARTESIAN_POINT ( 'NONE',  ( 7.031302189457115048, -1.093890586381388585, -0.8417396958425467091 ) ) ;
#46260=CARTESIAN_POINT ( 'NONE',  ( -0.2999999999999999889, 0.000000000000000000, 0.000000000000000000 ) ) ;
#46335=CARTESIAN_POINT ( 'NONE',  ( 6.965816936038000229, -1.147328252452000097, 0.8605332073374000190 ) ) ;
#46404=ADVANCED_FACE ( 'NONE', ( #28816, #39635 ), #60957, .T. ) ;
#46427=CARTESIAN_POINT ( 'NONE',  ( -0.2999999999999999889, 0.5773502691895999739, 1.000000000000000000 ) ) ;
#46447=CIRCLE ( 'NONE', #15191, 1.000000000000000000 ) ;
#46479=AXIS2_PLACEMENT_3D ( 'NONE', #39406, #33131, #6891 ) ;
#46510=CARTESIAN_POINT ( 'NONE',  ( 6.226007504534000425, 0.03883618666160999766, -1.614257485795999925 ) ) ;
#46530=CARTESIAN_POINT ( 'NONE',  ( 5.002606837613999602, -0.4199405305951999789, 1.440017343911000003 ) ) ;
#46592=CARTESIAN_POINT ( 'NONE',  ( 4.558531403101000912, 1.112796118072999940, -0.2204328748767000190 ) ) ;
#46637=CARTESIAN_POINT ( 'NONE',  ( 4.400023385887159577, -1.108947733447370521, -0.4820500775937197058 ) ) ;
#46649=AXIS2_PLACEMENT_3D ( 'NONE', #28629, #44368, #34217 ) ;
#46654=EDGE_CURVE ( 'NONE', #9931, #47471, #9849, .T. ) ;
#46672=CARTESIAN_POINT ( 'NONE',  ( 5.908316242380999839, -0.7225053299333999979, -0.9279906512076999681 ) ) ;
#46685=CARTESIAN_POINT ( 'NONE',  ( 5.392306792578000163, -0.7698221690009998674, -0.8891327474049000035 ) ) ;
#46711=B_SPLINE_CURVE_WITH_KNOTS ( 'NONE', 3,
 ( #19275, #45853, #36388, #52116, #68532, #4221, #51777, #36041, #51099, #62272 ),
 .UNSPECIFIED., .F., .F.,
 ( 4, 2, 2, 2, 4 ),
 ( 0.000000000000000000, 0.2500000000000000000, 0.5000000000000000000, 0.7500000000000000000, 1.000000000000000000 ),
 .UNSPECIFIED. ) ;
#46716=CARTESIAN_POINT ( 'NONE',  ( 0.7000000000000000666, 0.000000000000000000, 0.5999999999999999778 ) ) ;
#46745=CARTESIAN_POINT ( 'NONE',  ( 6.902955114085999710, 1.212008421426999938, 0.9737989909727998716 ) ) ;
#46793=EDGE_CURVE ( 'NONE', #49400, #4446, #52144, .T. ) ;
#46819=CARTESIAN_POINT ( 'NONE',  ( 7.278633126552175980, -0.8622146015440113054, 0.7572888212223023441 ) ) ;
#46830=CARTESIAN_POINT ( 'NONE',  ( 7.492862293499999993, -1.342370813310000077, 0.5333876762063000099 ) ) ;
#46886=VERTEX_POINT ( 'NONE', #49694 ) ;
#46897=EDGE_LOOP ( 'NONE', ( #23157, #26283, #63868, #44915 ) ) ;
#46931=CARTESIAN_POINT ( 'NONE',  ( 4.876954876535999794, -1.207493506464999866, 0.4107732707878000156 ) ) ;
#46974=B_SPLINE_CURVE_WITH_KNOTS ( 'NONE', 3,
 ( #21409, #27704, #10924, #5331, #22095, #4989, #53577, #36817, #31571, #5670, #27011, #64388, #54255, #49020, #43082, #16509, #26325, #53914, #37155 ),
 .UNSPECIFIED., .F., .F.,
 ( 4, 1, 1, 1, 1, 1, 1, 1, 1, 1, 1, 1, 1, 1, 1, 1, 4 ),
 ( 0.000000000000000000, 0.04500057695454640072, 0.1100005346419700436, 0.1750004923296970549, 0.2400004500171206978, 0.3050004077048477646, 0.3700003653922710467, 0.4350003230796946618, 0.5000002807674217564, 0.5650002384548453715, 0.6300001961425724106, 0.6950001538299960258, 0.7600001115177230648, 0.8250000692051463469, 0.8900000268925699620, 0.9549999845802970011, 1.000000000000000000 ),
 .UNSPECIFIED. ) ;
#46998=CARTESIAN_POINT ( 'NONE',  ( -0.2999999999999999889, 0.5773502691895999739, -1.000000000000000000 ) ) ;
#47012=CARTESIAN_POINT ( 'NONE',  ( 6.109973520848999584, 1.122942780917999928, 0.3495427174121999991 ) ) ;
#47023=CARTESIAN_POINT ( 'NONE',  ( 5.207454287316000574, -0.1144865814785000074, 1.118427654993999987 ) ) ;
#47048=CARTESIAN_POINT ( 'NONE',  ( 5.459193173017250267, 0.3926218265389159190, 1.460959015002474715 ) ) ;
#47055=CARTESIAN_POINT ( 'NONE',  ( 5.240124045625999649, 0.9801419917718999786, -1.210444677476000264 ) ) ;
#47087=CARTESIAN_POINT ( 'NONE',  ( 7.073405103028999719, 1.118341376545999966, -0.1779135255794999926 ) ) ;
#47128=EDGE_CURVE ( 'NONE', #39559, #7001, #4304, .T. ) ;
#47186=ORIENTED_EDGE ( 'NONE', *, *, #25918, .F. ) ;
#47193=ORIENTED_EDGE ( 'NONE', *, *, #8134, .F. ) ;
#47277=CARTESIAN_POINT ( 'NONE',  ( 4.500647932088999603, -0.4305483101668000079, -1.200584607419999950 ) ) ;
#47287=DIRECTION ( 'NONE',  ( -1.000000000000000000, 0.000000000000000000, 0.000000000000000000 ) ) ;
#47308=VERTEX_POINT ( 'NONE', #5327 ) ;
#47327=CARTESIAN_POINT ( 'NONE',  ( 0.2000000000000000389, -1.649999999999999911, 0.000000000000000000 ) ) ;
#47369=CARTESIAN_POINT ( 'NONE',  ( 5.493135431812000036, 0.6181797131151999247, -1.000516987031000005 ) ) ;
#47420=DIRECTION ( 'NONE',  ( 0.000000000000000000, 0.8660254037844288266, -0.5000000000000169864 ) ) ;
#47429=CARTESIAN_POINT ( 'NONE',  ( 6.936163246431000573, 0.7133195303071999671, 1.381457696855000084 ) ) ;
#47471=VERTEX_POINT ( 'NONE', #60891 ) ;
#47550=CARTESIAN_POINT ( 'NONE',  ( 5.782109839683332808, 0.9218200799623742503, -1.199500263597268912 ) ) ;
#47603=ADVANCED_FACE ( 'NONE', ( #3193 ), #24520, .T. ) ;
#47620=CARTESIAN_POINT ( 'NONE',  ( 4.774325709868000089, 0.05965109778420000369, 1.274055334230000058 ) ) ;
#47637=CARTESIAN_POINT ( 'NONE',  ( -0.2999999999999999889, 0.000000000000000000, 0.000000000000000000 ) ) ;
#47684=CARTESIAN_POINT ( 'NONE',  ( 5.959193173016666734, 0.3926218265389159190, 1.460959015002474715 ) ) ;
#47702=CARTESIAN_POINT ( 'NONE',  ( 6.607448840114000355, -0.9275392149503000061, 1.138410677097999812 ) ) ;
#47753=EDGE_CURVE ( 'NONE', #23416, #37303, #41076, .T. ) ;
#47782=CARTESIAN_POINT ( 'NONE',  ( 7.239445764754000479, -0.3967607077929999893, 1.060625802389000061 ) ) ;
#47811=CARTESIAN_POINT ( 'NONE',  ( 6.250859839683334584, 0.3926218265389220807, -1.460959015002473382 ) ) ;
#47837=EDGE_CURVE ( 'NONE', #54822, #62212, #21457, .T. ) ;
#47865=CARTESIAN_POINT ( 'NONE',  ( 6.795873790635000411, -1.061937232448999957, 0.3932159216488000375 ) ) ;
#47893=CARTESIAN_POINT ( 'NONE',  ( 5.750859839683333696, 0.3926218265389220807, -1.460959015002473382 ) ) ;
#47961=CARTESIAN_POINT ( 'NONE',  ( 4.603277098756000107, 1.034008087237999973, -0.7467278779783999010 ) ) ;
#47972=CARTESIAN_POINT ( 'NONE',  ( 4.813359839683166719, 1.310679582531387943, -0.7554284705563468760 ) ) ;
#47993=FACE_OUTER_BOUND ( 'NONE', #55264, .T. ) ;
#48024=CARTESIAN_POINT ( 'NONE',  ( 4.399638951366856787, 1.439362632458823121, 0.1347012276008314191 ) ) ;
#48025=CARTESIAN_POINT ( 'NONE',  ( 4.690443173016667799, 0.1963495408493637351, -1.499999999999999778 ) ) ;
#48038=CARTESIAN_POINT ( 'NONE',  ( 5.555416005062999929, 1.090514925437999993, -0.4404064970261999945 ) ) ;
#48082=CARTESIAN_POINT ( 'NONE',  ( 4.726978212288999615, 0.7677468988916000825, -1.355145506237000141 ) ) ;
#48115=CARTESIAN_POINT ( 'NONE',  ( 6.716245473203000138, -1.254186399022999998, -0.6529324254944000039 ) ) ;
#48121=LINE ( 'NONE', #226, #61298 ) ;
#48130=CARTESIAN_POINT ( 'NONE',  ( 5.252943173016666023, 1.199500263597271577, -0.9218200799623702535 ) ) ;
#48136=CARTESIAN_POINT ( 'NONE',  ( 6.945013804402999646, -1.256780975885000151, 0.6254553495446000255 ) ) ;
#48199=CARTESIAN_POINT ( 'NONE',  ( 6.961787026899999731, -0.7800294017036001337, -0.9775269195634000985 ) ) ;
#48215=ORIENTED_EDGE ( 'NONE', *, *, #6126, .F. ) ;
#48308=CARTESIAN_POINT ( 'NONE',  ( 4.688359839682667562, -0.7554284705563480973, -1.310679582531387277 ) ) ;
#48324=CARTESIAN_POINT ( 'NONE',  ( 6.310040576531521062, -1.097834706587868192, 0.2821293189078559194 ) ) ;
#48337=CARTESIAN_POINT ( 'NONE',  ( 4.555026506349999948, -1.500000000000000000, 0.000000000000000000 ) ) ;
#48348=CARTESIAN_POINT ( 'NONE',  ( 4.500442376531999855, 0.9099999783214999249, 1.169932331390999947 ) ) ;
#48381=CARTESIAN_POINT ( 'NONE',  ( 5.526874906801999998, 1.281289678559000000, 0.3267609307802000207 ) ) ;
#48408=CARTESIAN_POINT ( 'NONE',  ( 6.388158200622003235, 1.399447465758937303, 0.6237406411839149234 ) ) ;
#48424=CARTESIAN_POINT ( 'NONE',  ( 4.442764461075999982, -1.247736568755000164, 0.6705067152884000015 ) ) ;
#48426=B_SPLINE_CURVE_WITH_KNOTS ( 'NONE', 3,
 ( #27593, #5911, #10134, #48919, #10470, #47550, #68853, #47893, #42309, #1027, #5570, #64288, #48574, #42641, #32842, #41951, #4879, #63950 ),
 .UNSPECIFIED., .F., .F.,
 ( 4, 2, 2, 2, 2, 2, 2, 2, 4 ),
 ( 0.000000000000000000, 0.1250000000000000000, 0.2500000000000000000, 0.3750000000000000000, 0.5000000000000000000, 0.6250000000000000000, 0.7500000000000000000, 0.8750000000000000000, 1.000000000000000000 ),
 .UNSPECIFIED. ) ;
#48481=CARTESIAN_POINT ( 'NONE',  ( 5.903117865652999896, -0.8041423837011999476, 1.228772791746999937 ) ) ;
#48501=ORIENTED_EDGE ( 'NONE', *, *, #37497, .T. ) ;
#48522=CARTESIAN_POINT ( 'NONE',  ( 5.152393060466970987, -0.3471830745757842340, 1.190476739849418042 ) ) ;
#48545=ORIENTED_EDGE ( 'NONE', *, *, #7883, .T. ) ;
#48547=CARTESIAN_POINT ( 'NONE',  ( 7.028330717051000320, 0.9502619346694000102, -0.6159082020391000167 ) ) ;
#48554=CARTESIAN_POINT ( 'NONE',  ( 6.987460761722542379, -1.412538709148827731, 0.3006784195689278238 ) ) ;
#48574=CARTESIAN_POINT ( 'NONE',  ( 5.677943173016667622, -0.9218200799623716968, -1.199500263597270910 ) ) ;
#48648=CARTESIAN_POINT ( 'NONE',  ( 4.216434180875999971, -0.2452535255997999875, 1.107593380736000110 ) ) ;
#48670=CARTESIAN_POINT ( 'NONE',  ( 6.568578067412807364, 1.121778872040013253, -0.1568744671984653172 ) ) ;
#48702=CARTESIAN_POINT ( 'NONE',  ( 4.471808905520999744, 1.206178254336000233, -0.5711989167972000292 ) ) ;
#48718=CARTESIAN_POINT ( 'NONE',  ( 4.399695933186626995, 0.9886387176649684694, -0.8895061925674412340 ) ) ;
#48733=CARTESIAN_POINT ( 'NONE',  ( 5.353758726594999295, -1.146783406111000048, -0.2608682635935000160 ) ) ;
#48772=CARTESIAN_POINT ( 'NONE',  ( 4.374345016631999705, -0.3062339383746999766, 1.382988000970999831 ) ) ;
#48798=DIRECTION ( 'NONE',  ( 1.000000000000000000, 0.000000000000000000, 0.000000000000000000 ) ) ;
#48827=CARTESIAN_POINT ( 'NONE',  ( 6.205603783354000313, 1.388436026523999889, -0.4783021510498000062 ) ) ;
#48834=CARTESIAN_POINT ( 'NONE',  ( 6.146693173016666734, -1.310679582531386611, -0.7554284705563495406 ) ) ;
#48857=CARTESIAN_POINT ( 'NONE',  ( -0.2999999999999999889, 1.649999999999999911, 0.000000000000000000 ) ) ;
#48885=EDGE_CURVE ( 'NONE', #65585, #23416, #64784, .T. ) ;
#48894=CARTESIAN_POINT ( 'NONE',  ( 6.961659601440000067, -1.366112286775999829, -0.08575370944440000032 ) ) ;
#48896=CARTESIAN_POINT ( 'NONE',  ( 4.400000000000000355, 0.000000000000000000, 0.000000000000000000 ) ) ;
#48919=CARTESIAN_POINT ( 'NONE',  ( 5.813359839683332808, 1.310679582531387943, -0.7554284705563468760 ) ) ;
#49015=CARTESIAN_POINT ( 'NONE',  ( 5.550586697066033359, 1.058569194974100736, -0.4045265221279905066 ) ) ;
#49020=CARTESIAN_POINT ( 'NONE',  ( 6.901403243225498585, -0.7129370139181090416, -0.8934472489575943088 ) ) ;
#49026=VERTEX_POINT ( 'NONE', #29837 ) ;
#49043=CARTESIAN_POINT ( 'NONE',  ( 4.851842514214999902, 1.628762548987999992, 0.05628454206072999733 ) ) ;
#49071=CARTESIAN_POINT ( 'NONE',  ( 6.232675381438999906, -1.260983081135999884, 0.3979920142897999669 ) ) ;
#49111=CARTESIAN_POINT ( 'NONE',  ( 5.058539461080999722, -0.8103260286165000492, -1.161807459232000017 ) ) ;
#49144=CARTESIAN_POINT ( 'NONE',  ( 6.703706320014999775, -0.3939706863108000112, -1.504006644519000124 ) ) ;
#49163=CARTESIAN_POINT ( 'NONE',  ( 6.133316242380999483, -0.9919734638370999447, -1.274097314648999779 ) ) ;
#49172=B_SPLINE_CURVE_WITH_KNOTS ( 'NONE', 3,
 ( #45336, #66646, #8610, #34847, #8266, #51261, #36206, #57523, #25370, #41114, #47048, #19787, #5075, #52626, #56852, #26412, #57183, #25030 ),
 .UNSPECIFIED., .F., .F.,
 ( 4, 2, 2, 2, 2, 2, 2, 2, 4 ),
 ( 0.000000000000000000, 0.1250000000000000833, 0.2500000000000001665, 0.3750000000000001665, 0.5000000000000002220, 0.6250000000000002220, 0.7500000000000001110, 0.8750000000000001110, 1.000000000000000000 ),
 .UNSPECIFIED. ) ;
#49228=CARTESIAN_POINT ( 'NONE',  ( 7.160908395509999025, 1.148632353890999935, -0.7444811394398999083 ) ) ;
#49315=FACE_OUTER_BOUND ( 'NONE', #21295, .T. ) ;
#49344=ORIENTED_EDGE ( 'NONE', *, *, #979, .F. ) ;
#49351=CARTESIAN_POINT ( 'NONE',  ( 6.617053846953221630, 1.009847974094061351, 0.5132427797214026421 ) ) ;
#49379=CARTESIAN_POINT ( 'NONE',  ( 4.712147656733999490, -0.01772054397006999835, 1.186896354132999987 ) ) ;
#49400=VERTEX_POINT ( 'NONE', #8411 ) ;
#49413=CARTESIAN_POINT ( 'NONE',  ( 5.923521586833000896, 0.9584732047324999726, 1.299486219972000089 ) ) ;
#49497=EDGE_CURVE ( 'NONE', #13866, #95, #2471, .T. ) ;
#49508=CARTESIAN_POINT ( 'NONE',  ( 6.334973520849000117, 1.541759477651000187, 0.4799094010597000359 ) ) ;
#49513=ORIENTED_EDGE ( 'NONE', *, *, #54861, .F. ) ;
#49542=CARTESIAN_POINT ( 'NONE',  ( 7.150172442432219277, 1.249827089371011279, -0.1627375339325294601 ) ) ;
#49553=CARTESIAN_POINT ( 'NONE',  ( 6.666460567079824706, -1.086035832535817702, -1.060422689362632731 ) ) ;
#49619=CARTESIAN_POINT ( 'NONE',  ( 5.805026506351000037, 1.500000000000000000, 0.000000000000000000 ) ) ;
#49677=DIRECTION ( 'NONE',  ( 1.000000000000000000, 0.000000000000000000, -1.147230458784000007E-14 ) ) ;
#49694=CARTESIAN_POINT ( 'NONE',  ( 5.105026506350000659, -1.500000000000000000, 0.000000000000000000 ) ) ;
#49702=ORIENTED_EDGE ( 'NONE', *, *, #10087, .T. ) ;
#49734=CARTESIAN_POINT ( 'NONE',  ( 4.873530990069000701, -1.057166785643999907, -0.5398479887613999439 ) ) ;
#49742=CARTESIAN_POINT ( 'NONE',  ( 4.490432128704166637, -1.044347811062755982, 1.103919035642354940 ) ) ;
#49765=CARTESIAN_POINT ( 'NONE',  ( 5.570621349514000009, -1.512468930016000135, 0.5654847974100999375 ) ) ;
#49829=DIRECTION ( 'NONE',  ( 0.000000000000000000, -1.000000000000000000, 0.000000000000000000 ) ) ;
#49848=CARTESIAN_POINT ( 'NONE',  ( 7.051113898392529222, -0.6785257367072009549, -1.178968686944157129 ) ) ;
#49859=CARTESIAN_POINT ( 'NONE',  ( 5.896449988747999527, -0.7225053299333999979, -0.9279906512076999681 ) ) ;
#49876=FACE_OUTER_BOUND ( 'NONE', #221, .T. ) ;
#49896=ORIENTED_EDGE ( 'NONE', *, *, #53598, .F. ) ;
#49904=CARTESIAN_POINT ( 'NONE',  ( 6.777068426484442298, 0.8477796283345830908, -1.258946551967616179 ) ) ;
#49922=AXIS2_PLACEMENT_3D ( 'NONE', #7343, #55247, #13302 ) ;
#49964=CIRCLE ( 'NONE', #23162, 0.5999999999999999778 ) ;
#50101=VECTOR ( 'NONE', #37339, 1000.000000000000000 ) ;
#50117=CARTESIAN_POINT ( 'NONE',  ( 5.498333808541000955, 0.9320062393831999303, 1.134853260389000029 ) ) ;
#50149=CYLINDRICAL_SURFACE ( 'NONE', #36209, 1.500000000000000000 ) ;
#50210=CARTESIAN_POINT ( 'NONE',  ( 6.299764545682999817, -1.121550593885000113, 0.3539842735925000095 ) ) ;
#50251=CARTESIAN_POINT ( 'NONE',  ( 6.740199140016398971, 0.1957492585445249622, -1.505191492485322913 ) ) ;
#50277=EDGE_LOOP ( 'NONE', ( #61359, #64054, #38440, #68494 ) ) ;
#50299=EDGE_LOOP ( 'NONE', ( #68252, #33537, #17120, #11965 ) ) ;
#50308=CARTESIAN_POINT ( 'NONE',  ( -0.2999999999999999889, 0.000000000000000000, 0.000000000000000000 ) ) ;
#50323=CARTESIAN_POINT ( 'NONE',  ( 6.482109839683335650, -0.9218200799623778030, 1.199500263597266914 ) ) ;
#50454=CARTESIAN_POINT ( 'NONE',  ( 5.318549751428999883, 1.497237214918999859, -0.6046620561147000306 ) ) ;
#50551=CARTESIAN_POINT ( 'NONE',  ( 5.420847890839000094, -1.289352866216999960, -0.2932997125499000046 ) ) ;
#50608=ADVANCED_FACE ( 'NONE', ( #65375 ), #56280, .T. ) ;
#50662=EDGE_LOOP ( 'NONE', ( #5216, #62941 ) ) ;
#50672=CARTESIAN_POINT ( 'NONE',  ( 5.137494878958000832, -0.8910062039905000120, -1.277482911150999989 ) ) ;
#50675=ADVANCED_FACE ( 'NONE', ( #33578 ), #44769, .T. ) ;
#50719=CARTESIAN_POINT ( 'NONE',  ( 4.805026506350000837, 1.500000000000000000, 0.000000000000000000 ) ) ;
#50740=ORIENTED_EDGE ( 'NONE', *, *, #41270, .T. ) ;
#50792=DIRECTION ( 'NONE',  ( 0.000000000000000000, 0.5000000000000169864, -0.8660254037844288266 ) ) ;
#50848=VERTEX_POINT ( 'NONE', #60744 ) ;
#50886=DIRECTION ( 'NONE',  ( 0.000000000000000000, -1.000000000000000000, 0.000000000000000000 ) ) ;
#50895=CARTESIAN_POINT ( 'NONE',  ( 6.328305643943999748, -0.7806768893493000183, 1.067248597240000096 ) ) ;
#50898=CARTESIAN_POINT ( 'NONE',  ( 7.400000000000000355, 0.000000000000000000, -0.5999999999999999778 ) ) ;
#50910=CYLINDRICAL_SURFACE ( 'NONE', #45977, 2.149999999999999911 ) ;
#50955=CARTESIAN_POINT ( 'NONE',  ( 4.400000000000000355, 1.000000000000000000, 0.000000000000000000 ) ) ;
#50971=CARTESIAN_POINT ( 'NONE',  ( 5.200859839683333874, 0.3926218265389221362, -1.460959015002473160 ) ) ;
#51007=CARTESIAN_POINT ( 'NONE',  ( 6.325859839683334762, 1.460959015002472494, 0.3926218265389232465 ) ) ;
#51025=DIRECTION ( 'NONE',  ( 0.000000000000000000, -0.8660254037844288266, 0.5000000000000169864 ) ) ;
#51044=CARTESIAN_POINT ( 'NONE',  ( 5.366518311043334322, 1.085476820253131081, 1.060886400888860326 ) ) ;
#51054=ADVANCED_FACE ( 'NONE', ( #51963 ), #43287, .T. ) ;
#51089=CARTESIAN_POINT ( 'NONE',  ( 5.340524985724223406, -1.123086320356926793, -0.1487314272998045972 ) ) ;
#51099=CARTESIAN_POINT ( 'NONE',  ( 6.932475402859345159, 1.100779672715244351, 1.004415898055839973 ) ) ;
#51113=DIRECTION ( 'NONE',  ( 1.000000000000000000, 0.000000000000000000, 0.000000000000000000 ) ) ;
#51237=CARTESIAN_POINT ( 'NONE',  ( 5.550217628333999897, -0.9612325616298000863, -1.110208802542000051 ) ) ;
#51255=CARTESIAN_POINT ( 'NONE',  ( -0.2999999999999999889, 0.000000000000000000, 0.000000000000000000 ) ) ;
#51256=CARTESIAN_POINT ( 'NONE',  ( 4.400000000000000355, 0.000000000000000000, 0.000000000000000000 ) ) ;
#51261=CARTESIAN_POINT ( 'NONE',  ( 5.532109839683624131, -0.9218200799623775810, 1.199500263597266247 ) ) ;
#51344=ORIENTED_EDGE ( 'NONE', *, *, #40108, .F. ) ;
#51364=PLANE ( 'NONE',  #41752 ) ;
#51381=CARTESIAN_POINT ( 'NONE',  ( 7.293613499430000147, 1.437192322347000006, 0.3816175901828000039 ) ) ;
#51428=AXIS2_PLACEMENT_3D ( 'NONE', #36487, #28597, #57808 ) ;
#51479=CARTESIAN_POINT ( 'NONE',  ( 7.011490480521701762, -1.352039016092809298, -0.3642379411497885799 ) ) ;
#51498=CARTESIAN_POINT ( 'NONE',  ( 6.555026506349999948, -1.500000000000000000, 0.000000000000000000 ) ) ;
#51523=VECTOR ( 'NONE', #27716, 1000.000000000000000 ) ;
#51548=ORIENTED_EDGE ( 'NONE', *, *, #60533, .F. ) ;
#51558=CARTESIAN_POINT ( 'NONE',  ( 6.563702397401000255, 1.130384497037000058, -0.3246714051208999807 ) ) ;
#51608=EDGE_LOOP ( 'NONE', ( #12671, #8315, #58215, #37660, #49513, #12829 ) ) ;
#51648=CARTESIAN_POINT ( 'NONE',  ( 5.096693173016665135, -1.310679582531386389, -0.7554284705563492075 ) ) ;
#51651=EDGE_CURVE ( 'NONE', #9931, #14587, #52209, .T. ) ;
#51709=EDGE_CURVE ( 'NONE', #54265, #46886, #30582, .T. ) ;
#51722=CARTESIAN_POINT ( 'NONE',  ( 7.094364705359000212, -0.9274734728647999749, -1.162302709265000011 ) ) ;
#51727=EDGE_LOOP ( 'NONE', ( #23426, #45057, #27220, #2083 ) ) ;
#51743=CARTESIAN_POINT ( 'NONE',  ( 5.469792710280000136, 0.08722338096737999869, 1.612367018429999854 ) ) ;
#51777=CARTESIAN_POINT ( 'NONE',  ( 7.029903297284646690, 0.4289550007897103834, 1.323513554004721149 ) ) ;
#51792=CARTESIAN_POINT ( 'NONE',  ( 6.105026506350000659, -1.500000000000000000, 0.000000000000000000 ) ) ;
#51820=CARTESIAN_POINT ( 'NONE',  ( 5.037467514214999831, 1.016370699457000093, -0.5038814123657998634 ) ) ;
#51869=VECTOR ( 'NONE', #14407, 1000.000000000000000 ) ;
#51899=CARTESIAN_POINT ( 'NONE',  ( 6.009144881614999711, 0.6694104981402000387, -0.9669902716602000181 ) ) ;
#51912=CARTESIAN_POINT ( 'NONE',  ( 5.341892472960999783, -1.146783406111000048, -0.2608682635935000160 ) ) ;
#51945=CIRCLE ( 'NONE', #63114, 0.5000000000000000000 ) ;
#51962=FACE_OUTER_BOUND ( 'NONE', #68822, .T. ) ;
#51963=FACE_OUTER_BOUND ( 'NONE', #27929, .T. ) ;
#51970=CARTESIAN_POINT ( 'NONE',  ( 6.774531911923999949, -0.7882360144965000481, 0.7672747788395000157 ) ) ;
#51977=CARTESIAN_POINT ( 'NONE',  ( 6.954847353040172209, -0.9689943386775232703, 1.116583658536274948 ) ) ;
#52040=VERTEX_POINT ( 'NONE', #19668 ) ;
#52048=CARTESIAN_POINT ( 'NONE',  ( 7.167854234552727632, 1.232145303795026292, 0.2729883214974913597 ) ) ;
#52116=CARTESIAN_POINT ( 'NONE',  ( 7.159807156518384730, -0.4668129303315028400, 1.167714605286940488 ) ) ;
#52144=B_SPLINE_CURVE_WITH_KNOTS ( 'NONE', 3,
 ( #31899, #53212, #26655, #47972, #37472, #21391, #64029, #58800, #5651, #69, #26992, #48308, #415, #43422, #65417, #35009, #13342, #39208 ),
 .UNSPECIFIED., .F., .F.,
 ( 4, 2, 2, 2, 2, 2, 2, 2, 4 ),
 ( 0.000000000000000000, 0.1250000000000000000, 0.2500000000000000000, 0.3750000000000000000, 0.5000000000000000000, 0.6250000000000000000, 0.7500000000000000000, 0.8750000000000000000, 1.000000000000000000 ),
 .UNSPECIFIED. ) ;
#52166=CARTESIAN_POINT ( 'NONE',  ( 4.319063347543000475, -1.132153191583000096, 0.07165796951064999643 ) ) ;
#52176=CIRCLE ( 'NONE', #37704, 0.9999997023190999590 ) ;
#52179=DIRECTION ( 'NONE',  ( 0.000000000000000000, 0.000000000000000000, -1.000000000000000000 ) ) ;
#52186=CARTESIAN_POINT ( 'NONE',  ( 6.713407900711241716, 0.6189880680375690059, -1.392846009744216573 ) ) ;
#52209=CIRCLE ( 'NONE', #34367, 1.649999999999999911 ) ;
#52250=CARTESIAN_POINT ( 'NONE',  ( 6.765359675869000000, -0.7428381837956999911, 0.9117187782023999931 ) ) ;
#52251=CIRCLE ( 'NONE', #14295, 1.500000000000000000 ) ;
#52325=CARTESIAN_POINT ( 'NONE',  ( 7.048326796653999970, 0.08385301782618000133, 1.411478992815000000 ) ) ;
#52391=ORIENTED_EDGE ( 'NONE', *, *, #26616, .T. ) ;
#52451=MANIFOLD_SOLID_BREP ( 'Stock-MAS-678-1', #36975 ) ;
#52453=CARTESIAN_POINT ( 'NONE',  ( 0.2000000000000000389, 0.000000000000000000, 0.000000000000000000 ) ) ;
#52468=DIRECTION ( 'NONE',  ( 1.000000000000000000, 0.000000000000000000, 0.000000000000000000 ) ) ;
#52475=EDGE_CURVE ( 'NONE', #55564, #25719, #15084, .T. ) ;
#52510=CARTESIAN_POINT ( 'NONE',  ( 4.226970154309000804, 0.7404484344845000399, 0.9906202336981998480 ) ) ;
#52571=DIRECTION ( 'NONE',  ( 1.000000000000000000, 0.000000000000000000, -1.924386576027000187E-14 ) ) ;
#52626=CARTESIAN_POINT ( 'NONE',  ( 5.407109839684124175, 1.199500263597268246, 0.9218200799623752495 ) ) ;
#52632=CARTESIAN_POINT ( 'NONE',  ( 4.932236545624000712, 0.07284287022823998647, 1.555811222638000091 ) ) ;
#52666=CARTESIAN_POINT ( 'NONE',  ( 6.969371378776000547, 0.09220185020346000071, 1.552013010797000048 ) ) ;
#52693=CARTESIAN_POINT ( 'NONE',  ( 6.240443173016666734, 0.1963495408493638184, -1.499999999999999778 ) ) ;
#52767=UNCERTAINTY_MEASURE_WITH_UNIT (LENGTH_MEASURE( 1.000000000000000082E-05 ), #60580, 'distance_accuracy_value', 'NONE');
#52837=CARTESIAN_POINT ( 'NONE',  ( 4.490838406521878490, 0.5240408911627599808, -1.077889606989799409 ) ) ;
#52860=CARTESIAN_POINT ( 'NONE',  ( 4.945374320980000071, -1.099255157290000007, -0.6468487824790000174 ) ) ;
#52923=CARTESIAN_POINT ( 'NONE',  ( 6.032109839683332808, -0.9218200799623775810, 1.199500263597266247 ) ) ;
#52978=EDGE_LOOP ( 'NONE', ( #4711, #55120, #51548, #27891 ) ) ;
#52988=CARTESIAN_POINT ( 'NONE',  ( 5.271693173017333756, 0.7554284705563509839, -1.310679582531385945 ) ) ;
#53018=CARTESIAN_POINT ( 'NONE',  ( 7.015118664308999996, 0.6487287962077999959, 1.256367379015999930 ) ) ;
#53059=VERTEX_POINT ( 'NONE', #50955 ) ;
#53091=CARTESIAN_POINT ( 'NONE',  ( 7.234321569752399483, 0.04198228903204147960, 1.193235013897578245 ) ) ;
#53101=CARTESIAN_POINT ( 'NONE',  ( 6.862290055324999472, -1.004440062237000220, -0.5229138879281000074 ) ) ;
#53159=( LENGTH_UNIT ( ) NAMED_UNIT ( * ) SI_UNIT ( .MILLI., .METRE. ) );
#53201=CARTESIAN_POINT ( 'NONE',  ( 4.866418903102999849, -0.9777056432663999708, -0.5753238461295000494 ) ) ;
#53212=CARTESIAN_POINT ( 'NONE',  ( 4.844609839683289287, 1.500000000000000888, -0.1963495408493590444 ) ) ;
#53271=CARTESIAN_POINT ( 'NONE',  ( 4.805026506350000837, 1.500000000000000000, 0.000000000000000000 ) ) ;
#53286=CARTESIAN_POINT ( 'NONE',  ( 6.182261061822000414, -0.7806768893493000183, 1.067248597240000096 ) ) ;
#53304=CIRCLE ( 'NONE', #62238, 0.9999997023190999590 ) ;
#53310=EDGE_CURVE ( 'NONE', #95, #2054, #62389, .T. ) ;
#53331=CARTESIAN_POINT ( 'NONE',  ( 5.195378349970999565, 1.269083497910999947, -0.6291676704954000110 ) ) ;
#53362=CARTESIAN_POINT ( 'NONE',  ( 6.728784626390999613, -1.193958516581999918, 0.4421009869154999827 ) ) ;
#53398=LINE ( 'NONE', #22949, #29788 ) ;
#53447=CARTESIAN_POINT ( 'NONE',  ( 7.061538849395999407, 1.118341376545999966, -0.1779135255794999926 ) ) ;
#53513=DIRECTION ( 'NONE',  ( 1.000000000000000000, 0.000000000000000000, 0.000000000000000000 ) ) ;
#53577=CARTESIAN_POINT ( 'NONE',  ( 7.133860169640499294, 0.8910540846543333338, 0.7159253625619631523 ) ) ;
#53593=ORIENTED_EDGE ( 'NONE', *, *, #31763, .T. ) ;
#53597=CARTESIAN_POINT ( 'NONE',  ( 4.407312471546000587, -0.7071374513468999812, -0.8783066828273999871 ) ) ;
#53598=EDGE_CURVE ( 'NONE', #56839, #66643, #8270, .T. ) ;
#53608=CARTESIAN_POINT ( 'NONE',  ( 6.021693173016668510, -0.7554284705563544255, 1.310679582531384169 ) ) ;
#53628=CARTESIAN_POINT ( 'NONE',  ( 5.778946504885999147, -1.272350122907000003, -0.3600015818555999947 ) ) ;
#53668=CARTESIAN_POINT ( 'NONE',  ( 6.263359839683333874, 1.310679582531388387, -0.7554284705563470981 ) ) ;
#53673=CARTESIAN_POINT ( 'NONE',  ( 4.579603349966000714, -0.4781559447700999832, -1.333338567780000039 ) ) ;
#53724=CARTESIAN_POINT ( 'NONE',  ( 7.023969222280999958, -1.381912473529000041, 0.6877288610791999490 ) ) ;
#53781=CARTESIAN_POINT ( 'NONE',  ( 6.778816671981999775, -0.8882170986559999593, 0.6661914818925001036 ) ) ;
#53786=CARTESIAN_POINT ( 'NONE',  ( 3.400000000000000355, 0.000000000000000000, 0.000000000000000000 ) ) ;
#53787=CARTESIAN_POINT ( 'NONE',  ( 7.260532792544999836, 1.067048968730999858, 0.8573300240319000620 ) ) ;
#53810=EDGE_LOOP ( 'NONE', ( #19194, #36806, #62831, #13243 ) ) ;
#53858=CONICAL_SURFACE ( 'NONE', #4741, 1.200857723089999940, 0.7853979760808852406 ) ;
#53872=ORIENTED_EDGE ( 'NONE', *, *, #7883, .F. ) ;
#53908=CARTESIAN_POINT ( 'NONE',  ( 5.679855442506180907, 0.3526799806875357546, 1.076168297469421553 ) ) ;
#53914=CARTESIAN_POINT ( 'NONE',  ( 6.786452000648069749, -0.9523218012055599813, 0.5806051447938145316 ) ) ;
#53934=CARTESIAN_POINT ( 'NONE',  ( 4.930797932093000213, 1.481278897913000048, 0.05118800434419999712 ) ) ;
#53963=CARTESIAN_POINT ( 'NONE',  ( 6.557034520496999974, -0.07351275584480999881, 1.466703212027999914 ) ) ;
#53995=CARTESIAN_POINT ( 'NONE',  ( 7.400000000000000355, 0.000000000000000000, 0.5999999999999999778 ) ) ;
#54007=CARTESIAN_POINT ( 'NONE',  ( 4.305925572186999339, 0.8223230991370998888, 1.100157502810999999 ) ) ;
#54015=CARTESIAN_POINT ( 'NONE',  ( 4.417085542195750669, 1.094284481885183125, 1.075295689758499318 ) ) ;
#54063=CARTESIAN_POINT ( 'NONE',  ( 5.852703546036000404, 0.07932534654106999927, 1.466367974616999748 ) ) ;
#54127=CARTESIAN_POINT ( 'NONE',  ( 6.994867733785000041, -1.214120350334000120, -0.6320739451511001583 ) ) ;
#54131=LINE ( 'NONE', #5546, #1014 ) ;
#54165=ORIENTED_EDGE ( 'NONE', *, *, #17923, .T. ) ;
#54167=CARTESIAN_POINT ( 'NONE',  ( 5.565443173016707767, -1.500000000000000222, -0.1963495408493622363 ) ) ;
#54224=ORIENTED_EDGE ( 'NONE', *, *, #52475, .F. ) ;
#54225=ADVANCED_FACE ( 'NONE', ( #35496 ), #37851, .F. ) ;
#54249=CARTESIAN_POINT ( 'NONE',  ( 5.534428103885884020, 0.9514691251117015636, -0.6142997976039359376 ) ) ;
#54255=CARTESIAN_POINT ( 'NONE',  ( 6.934611375570498559, -0.2896425330593513925, -1.105727683284202678 ) ) ;
#54265=VERTEX_POINT ( 'NONE', #33694 ) ;
#54279=CARTESIAN_POINT ( 'NONE',  ( 4.995294366068000258, -0.4131193957761999935, 1.492006182730000186 ) ) ;
#54286=CARTESIAN_POINT ( 'NONE',  ( 4.412918875529167728, 0.3262666342505332051, 1.484200010477007226 ) ) ;
#54288=DIRECTION ( 'NONE',  ( 1.000000000000000000, 0.000000000000000000, 0.000000000000000000 ) ) ;
#54311=CARTESIAN_POINT ( 'NONE',  ( 5.505001685446000437, 0.6181797131151999247, -1.000516987031000005 ) ) ;
#54344=DIRECTION ( 'NONE',  ( 1.000000000000000000, 0.000000000000000000, 5.921189464682000602E-14 ) ) ;
#54351=CARTESIAN_POINT ( 'NONE',  ( 4.750651961078999896, 1.377769485253000248, 0.3289013390324999619 ) ) ;
#54412=CARTESIAN_POINT ( 'NONE',  ( 6.687873758168000116, 0.03883618666160999766, -1.614257485795999925 ) ) ;
#54448=ORIENTED_EDGE ( 'NONE', *, *, #14195, .T. ) ;
#54477=CARTESIAN_POINT ( 'NONE',  ( 7.061283998474999990, -0.3468507372608000128, -1.324123422434000164 ) ) ;
#54512=DIRECTION ( 'NONE',  ( 1.000000000000000000, 0.000000000000000000, 0.000000000000000000 ) ) ;
#54518=CARTESIAN_POINT ( 'NONE',  ( 4.400000000000000355, 0.000000000000000000, 0.000000000000000000 ) ) ;
#54521=CARTESIAN_POINT ( 'NONE',  ( 5.669609839683792174, -0.1963495408493606265, -1.500000000000000222 ) ) ;
#54569=DIRECTION ( 'NONE',  ( 0.000000000000000000, 0.000000000000000000, -1.000000000000000000 ) ) ;
#54591=B_SPLINE_CURVE_WITH_KNOTS ( 'NONE', 3,
 ( #24423, #1112, #22425, #29689 ),
 .UNSPECIFIED., .F., .F.,
 ( 4, 4 ),
 ( 0.000000000000000000, 1.000000000000000000 ),
 .UNSPECIFIED. ) ;
#54634=CARTESIAN_POINT ( 'NONE',  ( 4.769414598756999801, -0.6079694192054000412, -1.351744651493000049 ) ) ;
#54636=B_SPLINE_SURFACE_WITH_KNOTS ( 'NONE', 3, 3, ( 
 ( #34547, #55859, #3052, #47782, #14922, #15613, #10361, #32046, #47087, #20855, #41491, #21196, #42871, #26450, #42527, #41834, #69091, #36245, #51970 ),
 ( #63836, #36592, #62803, #42191, #15950, #10701, #57564, #4073, #31015, #63143, #57919, #37280, #63493, #30662, #36943, #31696, #53362, #15268, #9665 ),
 ( #9319, #10015, #68388, #58257, #52325, #53018, #5114, #26801, #58600, #5465, #20508, #64179, #4420, #25758, #48115, #25410, #16293, #218, #21536 ),
 ( #4762, #37616, #31353, #26104, #52666, #47429, #46745, #68050, #20164, #68738, #6141, #59980, #49144, #5798, #43913, #58948, #28173, #17688, #33770 ) ),
 .UNSPECIFIED., .F., .F., .F.,
 ( 4, 4 ),
 ( 4, 1, 1, 1, 1, 1, 1, 1, 1, 1, 1, 1, 1, 1, 1, 1, 4 ),
 ( -0.02636945251836000231, 1.026369452518000047 ),
 ( 0.6640607743075999103, 0.6854686661408999626, 0.7068765579742000149, 0.7282844498075999873, 0.7496923416409000396, 0.7711002334743000119, 0.7925081253075999532, 0.8139160171409000055, 0.8353239089742999779, 0.8567318008076000302, 0.8781396926410000026, 0.8995475844743000549, 0.9209554763077000272, 0.9423633681409999685, 0.9637712599743000208, 0.9851791518076999932, 1.006587043640999823 ),
 .UNSPECIFIED. ) ;
#54664=CARTESIAN_POINT ( 'NONE',  ( 6.405791561646000609, 1.411445953971000034, -0.4053984660343999957 ) ) ;
#54688=CARTESIAN_POINT ( 'NONE',  ( 6.553816671982000130, -1.199981415667000118, 0.9000247785775999931 ) ) ;
#54692=CARTESIAN_POINT ( 'NONE',  ( 4.909193173016666911, 0.3926218265389159745, 1.460959015002474493 ) ) ;
#54732=TOROIDAL_SURFACE ( 'NONE', #36864, 1.649999999999999911, 0.5000000000000000000 ) ;
#54757=CARTESIAN_POINT ( 'NONE',  ( 6.911404257992000311, -0.9275392149503000061, 1.138410677097999812 ) ) ;
#54765=VERTEX_POINT ( 'NONE', #14337 ) ;
#54766=CARTESIAN_POINT ( 'NONE',  ( 5.355026506350999860, 1.500000000000000000, 0.000000000000000000 ) ) ;
#54792=CARTESIAN_POINT ( 'NONE',  ( 5.909193173017250444, 0.3926218265389159745, 1.460959015002474493 ) ) ;
#54822=VERTEX_POINT ( 'NONE', #4167 ) ;
#54837=EDGE_CURVE ( 'NONE', #25728, #55564, #69125, .T. ) ;
#54861=EDGE_CURVE ( 'NONE', #23416, #3150, #54131, .T. ) ;
#54953=CARTESIAN_POINT ( 'NONE',  ( 6.697846812853917697, 0.1022963455632099478, 1.128078040366519597 ) ) ;
#54958=CARTESIAN_POINT ( 'NONE',  ( 0.7000000000000000666, 0.000000000000000000, 0.000000000000000000 ) ) ;
#54982=CARTESIAN_POINT ( 'NONE',  ( 4.310425572186999510, -0.9683957735725999827, -0.7692866548104999591 ) ) ;
#54990=SURFACE_STYLE_FILL_AREA ( #65110 ) ;
#55040=DIRECTION ( 'NONE',  ( 1.000000000000000000, 0.000000000000000000, 0.000000000000000000 ) ) ;
#55106=CARTESIAN_POINT ( 'NONE',  ( 6.738288077784000407, 0.9869232226998000401, -1.278013103562000152 ) ) ;
#55120=ORIENTED_EDGE ( 'NONE', *, *, #37864, .F. ) ;
#55139=CARTESIAN_POINT ( 'NONE',  ( 6.002943173016874745, -1.199500263597274241, 0.9218200799623669228 ) ) ;
#55200=EDGE_CURVE ( 'NONE', #6243, #56839, #36483, .T. ) ;
#55209=CARTESIAN_POINT ( 'NONE',  ( 5.036746727192666029, -1.006919573152100789, 1.157429495210549941 ) ) ;
#55247=DIRECTION ( 'NONE',  ( 1.000000000000000000, 0.000000000000000000, 0.000000000000000000 ) ) ;
#55259=CARTESIAN_POINT ( 'NONE',  ( 5.428010115736667807, 0.04029576578756271371, 1.517272597181324567 ) ) ;
#55264=EDGE_LOOP ( 'NONE', ( #19290, #41607, #58751, #14739, #63823, #22285 ) ) ;
#55306=DIRECTION ( 'NONE',  ( -1.000000000000000000, 0.000000000000000000, 0.000000000000000000 ) ) ;
#55335=SURFACE_STYLE_USAGE ( .BOTH. , #12685 ) ;
#55358=CARTESIAN_POINT ( 'NONE',  ( 5.901648365476000357, 1.388436026523999889, -0.4783021510498000062 ) ) ;
#55390=DIRECTION ( 'NONE',  ( 0.000000000000000000, -1.000000000000000000, 0.000000000000000000 ) ) ;
#55402=EDGE_CURVE ( 'NONE', #52040, #63838, #48121, .T. ) ;
#55454=CARTESIAN_POINT ( 'NONE',  ( 5.370433571222000602, -1.212815126404999999, 0.5269083208682000530 ) ) ;
#55467=ORIENTED_EDGE ( 'NONE', *, *, #63602, .F. ) ;
#55486=CARTESIAN_POINT ( 'NONE',  ( 6.034193173016747735, -1.460959015002474493, 0.3926218265389144757 ) ) ;
#55509=TOROIDAL_SURFACE ( 'NONE', #64410, 1.649999999999999911, 0.5000000000000000000 ) ;
#55510=B_SPLINE_CURVE_WITH_KNOTS ( 'NONE', 3,
 ( #11351, #33384, #11694, #21840, #58912, #21163, #42490, #58562, #64140, #16255, #64825, #11015, #32352, #38269, #53668, #5760, #43174, #27103 ),
 .UNSPECIFIED., .F., .F.,
 ( 4, 2, 2, 2, 2, 2, 2, 2, 4 ),
 ( 0.000000000000000000, 0.1250000000000000000, 0.2500000000000000000, 0.3750000000000000000, 0.5000000000000000000, 0.6250000000000000000, 0.7500000000000000000, 0.8750000000000000000, 1.000000000000000000 ),
 .UNSPECIFIED. ) ;
#55532=VECTOR ( 'NONE', #31475, 1000.000000000000000 ) ;
#55559=CARTESIAN_POINT ( 'NONE',  ( 5.105026506350000659, -1.500000000000000000, 0.000000000000000000 ) ) ;
#55564=VERTEX_POINT ( 'NONE', #12099 ) ;
#55569=CARTESIAN_POINT ( 'NONE',  ( 6.388359839683332098, 0.7554284705563452107, 1.310679582531388609 ) ) ;
#55577=EDGE_CURVE ( 'NONE', #65623, #41499, #38083, .T. ) ;
#55644=AXIS2_PLACEMENT_3D ( 'NONE', #31949, #16544, #22133 ) ;
#55680=CARTESIAN_POINT ( 'NONE',  ( 4.744253625325000279, 0.4084786803018999879, -1.577726830116000123 ) ) ;
#55708=CARTESIAN_POINT ( 'NONE',  ( 5.873107267216000515, 1.541759477651000187, 0.4799094010597000359 ) ) ;
#55751=CARTESIAN_POINT ( 'NONE',  ( -0.2999999999999999889, 0.5773502691895999739, -1.000000000000000000 ) ) ;
#55760=CARTESIAN_POINT ( 'NONE',  ( 5.305026506349999948, 1.500000000000000000, 0.000000000000000000 ) ) ;
#55801=CARTESIAN_POINT ( 'NONE',  ( 5.723333808541000600, 0.8392109641639000639, 1.021861505418000027 ) ) ;
#55844=CARTESIAN_POINT ( 'NONE',  ( 6.998282674564999972, -1.401716800305999877, -2.564925509195000141E-10 ) ) ;
#55859=CARTESIAN_POINT ( 'NONE',  ( 7.294792651996000465, -0.9657653571052000618, 0.5483950127678999253 ) ) ;
#55907=ORIENTED_EDGE ( 'NONE', *, *, #60533, .T. ) ;
#55914=CARTESIAN_POINT ( 'NONE',  ( 6.471693173016667799, -0.7554284705563540925, 1.310679582531384391 ) ) ;
#55985=B_SPLINE_CURVE_WITH_KNOTS ( 'NONE', 3,
 ( #5862, #48522, #632, #17041 ),
 .UNSPECIFIED., .F., .F.,
 ( 4, 4 ),
 ( 0.000000000000000000, 1.000000000000000000 ),
 .UNSPECIFIED. ) ;
#55990=ADVANCED_FACE ( 'NONE', ( #2472 ), #13662, .T. ) ;
#56041=EDGE_CURVE ( 'NONE', #6927, #49400, #1786, .T. ) ;
#56047=LINE ( 'NONE', #2903, #62145 ) ;
#56057=CARTESIAN_POINT ( 'NONE',  ( 6.612810627809117214, -1.144927662556009196, -1.005512116229802189 ) ) ;
#56069=CARTESIAN_POINT ( 'NONE',  ( -0.2999999999999999889, -0.5773502691895999739, 1.000000000000000000 ) ) ;
#56098=EDGE_CURVE ( 'NONE', #68689, #59129, #52251, .T. ) ;
#56137=CARTESIAN_POINT ( 'NONE',  ( 5.874576767391999965, -1.238562288345000040, 0.4630760545261999872 ) ) ;
#56176=VECTOR ( 'NONE', #30282, 1000.000000000000000 ) ;
#56215=CARTESIAN_POINT ( 'NONE',  ( 5.138359839683333874, -0.7554284705563483193, -1.310679582531387721 ) ) ;
#56261=EDGE_LOOP ( 'NONE', ( #59397, #30437, #18613, #27974, #31339 ) ) ;
#56280=CYLINDRICAL_SURFACE ( 'NONE', #24273, 1.500000000000000000 ) ;
#56306=CARTESIAN_POINT ( 'NONE',  ( 1.700000000000000178, 0.000000000000000000, 0.000000000000000000 ) ) ;
#56333=ORIENTED_EDGE ( 'NONE', *, *, #46654, .F. ) ;
#56335=CARTESIAN_POINT ( 'NONE',  ( 5.259732019823497140, -0.7229411925607095446, 0.8718313054307640364 ) ) ;
#56343=B_SPLINE_CURVE_WITH_KNOTS ( 'NONE', 3,
 ( #40375, #13815, #64088, #5711, #68648, #42437, #15176, #4333, #27052, #48025, #15525, #63748, #36852, #41749, #10965, #10614, #31955, #53271 ),
 .UNSPECIFIED., .F., .F.,
 ( 4, 2, 2, 2, 2, 2, 2, 2, 4 ),
 ( 0.000000000000000000, 0.1250000000000000000, 0.2500000000000000000, 0.3750000000000000000, 0.5000000000000000000, 0.6250000000000000000, 0.7500000000000000000, 0.8750000000000000000, 1.000000000000000000 ),
 .UNSPECIFIED. ) ;
#56344=CARTESIAN_POINT ( 'NONE',  ( 3.400000000000000355, 1.000000000000000000, 0.000000000000000000 ) ) ;
#56364=CARTESIAN_POINT ( 'NONE',  ( 4.798048069770000090, 1.305799815673000186, -0.9751758809245999471 ) ) ;
#56476=CARTESIAN_POINT ( 'NONE',  ( 6.605026506349999771, -1.500000000000000000, 0.000000000000000000 ) ) ;
#56481=CARTESIAN_POINT ( 'NONE',  ( 5.997278627981999399, 0.6694104981402000387, -0.9669902716602000181 ) ) ;
#56519=VERTEX_POINT ( 'NONE', #27854 ) ;
#56623=AXIS2_PLACEMENT_3D ( 'NONE', #29582, #13151, #50886 ) ;
#56707=CARTESIAN_POINT ( 'NONE',  ( 4.400000000000000355, -1.000000000000000000, 0.000000000000000000 ) ) ;
#56743=PRODUCT ( '510 Connector Pin', '510 Connector Pin', '', ( #62741 ) ) ;
#56784=CARTESIAN_POINT ( 'NONE',  ( 4.400020611144109139, -0.9303305181083711961, -0.7135878619021024383 ) ) ;
#56805=DIRECTION ( 'NONE',  ( 0.000000000000000000, 1.000000000000000000, 0.000000000000000000 ) ) ;
#56818=CARTESIAN_POINT ( 'NONE',  ( 6.614116717018000635, 1.103230901197000069, 0.4075104821199000416 ) ) ;
#56828=CARTESIAN_POINT ( 'NONE',  ( 6.652664783001999815, 0.6479012572794000668, 0.9815235057283998588 ) ) ;
#56839=VERTEX_POINT ( 'NONE', #46335 ) ;
#56847=DIRECTION ( 'NONE',  ( -1.000000000000000000, 0.000000000000000000, 0.000000000000000000 ) ) ;
#56852=CARTESIAN_POINT ( 'NONE',  ( 5.396693173017498957, 1.310679582531385279, 0.7554284705563519831 ) ) ;
#56905=ORIENTED_EDGE ( 'NONE', *, *, #39500, .F. ) ;
#56971=CARTESIAN_POINT ( 'NONE',  ( 7.160780970049000160, 0.2385410637492000052, -1.467737005547999907 ) ) ;
#56991=CARTESIAN_POINT ( 'NONE',  ( 5.621035669130999501, -1.553728905769999891, -0.4396155223175000071 ) ) ;
#57082=CARTESIAN_POINT ( 'NONE',  ( 7.399999923048000028, 0.000000000000000000, 0.000000000000000000 ) ) ;
#57099=CARTESIAN_POINT ( 'NONE',  ( 5.002943173016664247, -1.199500263597274241, 0.9218200799623669228 ) ) ;
#57183=CARTESIAN_POINT ( 'NONE',  ( 5.365443173017625966, 1.500000000000000000, 0.1963495408493652339 ) ) ;
#57209=DIRECTION ( 'NONE',  ( -1.000000000000000000, 0.000000000000000000, 0.000000000000000000 ) ) ;
#57242=EDGE_LOOP ( 'NONE', ( #59438, #13230, #3687, #17993 ) ) ;
#57326=CARTESIAN_POINT ( 'NONE',  ( 5.671449988747999882, -0.9919734638370999447, -1.274097314648999779 ) ) ;
#57393=AXIS2_PLACEMENT_3D ( 'NONE', #68914, #10878, #58092 ) ;
#57405=CARTESIAN_POINT ( 'NONE',  ( 4.387482791987999953, -0.7931398200715998881, -0.8110703280130999726 ) ) ;
#57431=EDGE_CURVE ( 'NONE', #25079, #24359, #56047, .T. ) ;
#57447=CARTESIAN_POINT ( 'NONE',  ( 4.400031710115373862, -1.251998559788349619, 0.3836858220209141135 ) ) ;
#57472=ORIENTED_EDGE ( 'NONE', *, *, #21523, .T. ) ;
#57523=CARTESIAN_POINT ( 'NONE',  ( 5.500859839683752028, -0.3926218265389255779, 1.460959015002472494 ) ) ;
#57531=CARTESIAN_POINT ( 'NONE',  ( 5.344609839684291153, 1.500000000000000888, -0.1963495408493590444 ) ) ;
#57554=DIRECTION ( 'NONE',  ( 0.000000000000000000, 0.000000000000000000, -1.000000000000000000 ) ) ;
#57564=CARTESIAN_POINT ( 'NONE',  ( 7.060865949841000244, 0.9925148835426000904, 0.7974449476027000161 ) ) ;
#57582=ORIENTED_EDGE ( 'NONE', *, *, #23124, .T. ) ;
#57583=FACE_OUTER_BOUND ( 'NONE', #19515, .T. ) ;
#57611=VECTOR ( 'NONE', #25378, 1000.000000000000000 ) ;
#57649=CARTESIAN_POINT ( 'NONE',  ( 7.459654161154999130, -1.040770095916999871, 1.062041426571000091 ) ) ;
#57750=CARTESIAN_POINT ( 'NONE',  ( 5.287471543204999236, -0.1506867338748000273, 1.266511664267000015 ) ) ;
#57808=DIRECTION ( 'NONE',  ( 0.000000000000000000, 0.8445101382956362590, 0.5355395655933231636 ) ) ;
#57883=CARTESIAN_POINT ( 'NONE',  ( 5.000655990069000190, -1.131303444065999919, 1.070517240248999968 ) ) ;
#57919=CARTESIAN_POINT ( 'NONE',  ( 6.928033420461000347, 0.6960533226924000560, -1.066074183599000191 ) ) ;
#57946=CARTESIAN_POINT ( 'NONE',  ( 6.313359839683334584, 1.310679582531387943, -0.7554284705563468760 ) ) ;
#58024=VERTEX_POINT ( 'NONE', #66633 ) ;
#58047=EDGE_LOOP ( 'NONE', ( #10044, #30329, #18127, #4723 ) ) ;
#58049=FACE_OUTER_BOUND ( 'NONE', #37298, .T. ) ;
#58092=DIRECTION ( 'NONE',  ( 0.000000000000000000, 1.000000000000000000, 0.000000000000000000 ) ) ;
#58105=CARTESIAN_POINT ( 'NONE',  ( 4.842745154312999567, -0.9264254985263000730, 0.8766476166769999745 ) ) ;
#58196=DIRECTION ( 'NONE',  ( 0.000000000000000000, 0.5000000000000169864, 0.8660254037844288266 ) ) ;
#58209=VERTEX_POINT ( 'NONE', #54766 ) ;
#58215=ORIENTED_EDGE ( 'NONE', *, *, #66656, .F. ) ;
#58252=AXIS2_PLACEMENT_3D ( 'NONE', #56069, #8179, #55040 ) ;
#58257=CARTESIAN_POINT ( 'NONE',  ( 7.081534928999000833, -0.4954122222813999721, 1.324342293603000043 ) ) ;
#58311=CARTESIAN_POINT ( 'NONE',  ( 7.103945121988524569, 0.6535162433261614279, -1.132143873356089570 ) ) ;
#58340=CARTESIAN_POINT ( 'NONE',  ( 7.282926398363001042, -0.9657653571052000618, 0.5483950127678999253 ) ) ;
#58343=DIRECTION ( 'NONE',  ( 1.000000000000000000, 0.000000000000000000, 0.000000000000000000 ) ) ;
#58346=AXIS2_PLACEMENT_3D ( 'NONE', #54958, #55306, #23487 ) ;
#58350=PRODUCT_DEFINITION_CONTEXT ( 'detailed design', #39623, 'design' ) ;
#58418=CARTESIAN_POINT ( 'NONE',  ( 4.974988406525884699, 0.3003884035085989668, -1.160233976767930386 ) ) ;
#58444=CARTESIAN_POINT ( 'NONE',  ( 5.048003487648000664, 0.3164883147558000265, -1.235560760781999834 ) ) ;
#58476=ORIENTED_EDGE ( 'NONE', *, *, #19676, .T. ) ;
#58523=CARTESIAN_POINT ( 'NONE',  ( 6.204134283177999976, -1.390318139369000061, -0.4728033673814999727 ) ) ;
#58562=CARTESIAN_POINT ( 'NONE',  ( 6.159193173016667799, -0.3926218265389189721, -1.460959015002473604 ) ) ;
#58566=CARTESIAN_POINT ( 'NONE',  ( 4.863817101178999458, 1.226378114769999916, 0.9601309097413999183 ) ) ;
#58600=CARTESIAN_POINT ( 'NONE',  ( 6.915494267272999984, 1.396408403708000012, -0.2221503625482000033 ) ) ;
#58656=CARTESIAN_POINT ( 'NONE',  ( 7.110549024909053273, 0.7930388321308440291, -1.030519542554439560 ) ) ;
#58681=CARTESIAN_POINT ( 'NONE',  ( 1.700000000000000178, -1.500000000000000000, 0.000000000000000000 ) ) ;
#58719=ORIENTED_EDGE ( 'NONE', *, *, #55200, .F. ) ;
#58751=ORIENTED_EDGE ( 'NONE', *, *, #5034, .T. ) ;
#58786=CARTESIAN_POINT ( 'NONE',  ( 4.261179876531000055, 0.2683639413831000464, 1.246891768540999923 ) ) ;
#58800=CARTESIAN_POINT ( 'NONE',  ( 4.750859839682917141, 0.3926218265389220807, -1.460959015002473382 ) ) ;
#58837=CARTESIAN_POINT ( 'NONE',  ( 4.443175434508999544, -0.2631654914794999689, -1.157398794349000060 ) ) ;
#58854=CARTESIAN_POINT ( 'NONE',  ( 4.399736634486760778, 0.3091794154604233236, -1.210059008288320470 ) ) ;
#58872=CARTESIAN_POINT ( 'NONE',  ( 5.857901922764000346, -1.131660731475000015, -0.3201946116248999830 ) ) ;
#58901=CARTESIAN_POINT ( 'NONE',  ( 6.421289894894001371, 1.034288144986173608, 1.130377649294558973 ) ) ;
#58904=CARTESIAN_POINT ( 'NONE',  ( -0.2999999999999999889, 1.154700538379000108, 0.000000000000000000 ) ) ;
#58912=CARTESIAN_POINT ( 'NONE',  ( 6.107109839683332986, -1.199500263597270244, -0.9218200799623728070 ) ) ;
#58915=CARTESIAN_POINT ( 'NONE',  ( 4.879623228227333520, 1.445318020077273502, 0.4634605740919915950 ) ) ;
#58917=CARTESIAN_POINT ( 'NONE',  ( 4.784861683301000923, 1.115330177132999978, 0.8731915261176000920 ) ) ;
#58948=CARTESIAN_POINT ( 'NONE',  ( 6.604081922979999852, -1.551699729542000084, -0.09740341920656001018 ) ) ;
#58970=CARTESIAN_POINT ( 'NONE',  ( 5.730001685446000081, 0.8487381973356000753, -1.373673328256999948 ) ) ;
#59034=CARTESIAN_POINT ( 'NONE',  ( 7.194243953316000528, 0.9749085416657999881, 0.7832989749747000241 ) ) ;
#59066=B_SPLINE_SURFACE_WITH_KNOTS ( 'NONE', 3, 3, ( 
 ( #20476, #45430, #63459, #8021, #36214, #2771, #9634, #25722, #47055, #29359, #41804, #50672, #13619, #34942, #63107, #57883, #9984, #52632, #11699, #58566, #32357, #880, #16260, #48082, #16941, #185, #5431, #12056, #33039, #5766, #64145, #38274, #43874, #10671, #26771 ),
 ( #64484, #1222, #27108, #531, #64831, #22196, #32017, #53331, #43532, #22535, #21503, #49111, #65180, #59601, #37584, #11020, #32694, #16606, #42836, #58917, #54351, #17299, #6455, #37931, #38624, #53673, #27805, #59945, #59250, #48424, #21845, #48772, #11356, #43179, #54007 ),
 ( #6109, #27448, #57750, #16139, #10207, #68577, #9862, #4268, #31540, #58444, #30852, #26644, #52860, #68931, #46931, #58105, #59, #47620, #21045, #42377, #15460, #37462, #47961, #15113, #25944, #47277, #41340, #63682, #20700, #15797, #10546, #25604, #58786, #67898, #52510 ),
 ( #4960, #21382, #68234, #26294, #42029, #20016, #36785, #51820, #37126, #31890, #42714, #20356, #53201, #36433, #64018, #4610, #41679, #5302, #62653, #63331, #3918, #46592, #10892, #25254, #14773, #36091, #57405, #9510, #52166, #62984, #31206, #48648, #11925, #11233, #21718 ) ),
 .UNSPECIFIED., .F., .F., .F.,
 ( 4, 4 ),
 ( 4, 1, 1, 1, 1, 1, 1, 1, 1, 1, 1, 1, 1, 1, 1, 1, 1, 1, 1, 1, 1, 1, 1, 1, 1, 1, 1, 1, 1, 1, 1, 1, 4 ),
 ( -0.02636945251836000231, 1.026369452518000047 ),
 ( -0.01357143068969000020, 0.008482144181056000543, 0.03053571905179999768, 0.05258929392254999696, 0.07464286879330001012, 0.09669644366403999658, 0.1187500185347999948, 0.1408035934054999994, 0.1628571682763000072, 0.1849107431469999840, 0.2069643180178000197, 0.2290178928884999965, 0.2510714677593000044, 0.2731250426299999812, 0.2951786175007999891, 0.3172321923715000214, 0.3392857672423000293, 0.3613393421130000061, 0.3833929169837999584, 0.4054464918545000462, 0.4275000667252000230, 0.4495536415960000309, 0.4716072164667000077, 0.4936607913374999601, 0.5157143662081999924, 0.5377679410790000558, 0.5598215159496999771, 0.5818750908205000405, 0.6039286656911999618, 0.6259822405620000252, 0.6480358154326999465, 0.6700893903035000099, 0.6921429651742000422 ),
 .UNSPECIFIED. ) ;
#59088=( LENGTH_UNIT ( ) NAMED_UNIT ( * ) SI_UNIT ( .MILLI., .METRE. ) );
#59107=CARTESIAN_POINT ( 'NONE',  ( 5.082577295415885210, 1.197764792580507054, 0.04139071277677507793 ) ) ;
#59112=EDGE_CURVE ( 'NONE', #6243, #27153, #37775, .T. ) ;
#59129=VERTEX_POINT ( 'NONE', #35096 ) ;
#59147=ORIENTED_EDGE ( 'NONE', *, *, #33312, .F. ) ;
#59154=CARTESIAN_POINT ( 'NONE',  ( 5.696014035686344457, 0.1224074471714921564, 1.126874554618065849 ) ) ;
#59184=CARTESIAN_POINT ( 'NONE',  ( 4.418014461077000021, 0.5835563493861999351, -1.200305805718000274 ) ) ;
#59192=CARTESIAN_POINT ( 'NONE',  ( 1.700000000000000178, 0.000000000000000000, 0.000000000000000000 ) ) ;
#59210=CARTESIAN_POINT ( 'NONE',  ( 5.140365123072000664, -0.1287196877685000129, 1.257471894813999791 ) ) ;
#59236=CARTESIAN_POINT ( 'NONE',  ( 6.355026506350000659, 1.500000000000000000, 0.000000000000000000 ) ) ;
#59250=CARTESIAN_POINT ( 'NONE',  ( 4.476974183299000210, -1.413654420883999840, 0.08947517539409000076 ) ) ;
#59255=EDGE_CURVE ( 'NONE', #40685, #7462, #29514, .T. ) ;
#59270=EDGE_LOOP ( 'NONE', ( #37948, #39103, #29746, #50740, #42967 ) ) ;
#59306=CARTESIAN_POINT ( 'NONE',  ( 6.659332659907000185, 0.8975578082598999474, -1.162289642979999815 ) ) ;
#59397=ORIENTED_EDGE ( 'NONE', *, *, #25174, .T. ) ;
#59409=CARTESIAN_POINT ( 'NONE',  ( 5.227606837614000135, -0.3108367803229999948, 1.065889863396000115 ) ) ;
#59413=CARTESIAN_POINT ( 'NONE',  ( 5.690443173017207812, 0.1963495408493637351, -1.499999999999999778 ) ) ;
#59438=ORIENTED_EDGE ( 'NONE', *, *, #46654, .T. ) ;
#59487=ORIENTED_EDGE ( 'NONE', *, *, #31453, .F. ) ;
#59497=CARTESIAN_POINT ( 'NONE',  ( 5.889917153847927800, -0.8233002406113282268, -0.7791036658657048974 ) ) ;
#59501=DIRECTION ( 'NONE',  ( 0.000000000000000000, -1.000000000000000000, 0.000000000000000000 ) ) ;
#59527=LINE ( 'NONE', #66151, #36254 ) ;
#59529=CARTESIAN_POINT ( 'NONE',  ( 4.231470154306000708, -1.075475585643000054, -0.8543500892798999713 ) ) ;
#59557=CARTESIAN_POINT ( 'NONE',  ( 5.426046267568000125, 0.6950325411885999172, -1.124902434106000104 ) ) ;
#59571=CARTESIAN_POINT ( 'NONE',  ( 0.7000000000000000666, 0.000000000000000000, -0.5999999999999999778 ) ) ;
#59601=CARTESIAN_POINT ( 'NONE',  ( 4.990120016635999356, -1.409123102148000184, -0.1442114013433999919 ) ) ;
#59629=CARTESIAN_POINT ( 'NONE',  ( 0.7000000000000000666, -0.5773502691895999739, 1.000000000000000000 ) ) ;
#59643=CARTESIAN_POINT ( 'NONE',  ( 7.024698286478646025, -1.201388655186206300, -0.6934264365339433134 ) ) ;
#59656=CARTESIAN_POINT ( 'NONE',  ( 6.508089701055999932, -1.390318139369000061, -0.4728033673814999727 ) ) ;
#59679=EDGE_CURVE ( 'NONE', #6927, #54265, #15244, .T. ) ;
#59719=CARTESIAN_POINT ( 'NONE',  ( 6.840023874967999795, -0.9883789325241000290, 0.7262708681523000198 ) ) ;
#59723=ORIENTED_EDGE ( 'NONE', *, *, #47753, .T. ) ;
#59736=EDGE_LOOP ( 'NONE', ( #31458, #61197, #55467, #48501 ) ) ;
#59761=CARTESIAN_POINT ( 'NONE',  ( 5.794609839684291330, 1.500000000000001110, -0.1963495408493590721 ) ) ;
#59776=SURFACE_STYLE_FILL_AREA ( #22370 ) ;
#59844=CARTESIAN_POINT ( 'NONE',  ( 5.437476544805053713, -0.2480724261212651216, -1.105189088554211274 ) ) ;
#59854=CARTESIAN_POINT ( 'NONE',  ( 5.555026506349999948, -1.500000000000000000, 0.000000000000000000 ) ) ;
#59873=CARTESIAN_POINT ( 'NONE',  ( 4.328357053668000276, -0.7950496099306999520, -0.9874988013310997959 ) ) ;
#59880=CARTESIAN_POINT ( 'NONE',  ( 4.451675502116665406, -0.4062801362093708679, 1.464321016255251795 ) ) ;
#59905=CARTESIAN_POINT ( 'NONE',  ( 5.577289226418999490, 0.8392109641639000639, 1.021861505418000027 ) ) ;
#59945=CARTESIAN_POINT ( 'NONE',  ( 4.511183905521000348, -1.322317977380999876, -0.5078386052281999019 ) ) ;
#59980=CARTESIAN_POINT ( 'NONE',  ( 6.736914452361000727, 0.2494103027241000026, -1.534615152291000095 ) ) ;
#60002=CARTESIAN_POINT ( 'NONE',  ( 6.637459438551000623, -0.9243234316805000184, -1.323994513613999890 ) ) ;
#60022=CARTESIAN_POINT ( 'NONE',  ( 5.302805487806614870, -0.3471608085200784677, 1.190492330534066445 ) ) ;
#60039=EDGE_LOOP ( 'NONE', ( #33482, #30023 ) ) ;
#60055=AXIS2_PLACEMENT_3D ( 'NONE', #24376, #57209, #57554 ) ;
#60072=EDGE_LOOP ( 'NONE', ( #59723, #40518, #44642, #32152 ) ) ;
#60121=VECTOR ( 'NONE', #54344, 1000.000000000000000 ) ;
#60150=VECTOR ( 'NONE', #12503, 1000.000000000000000 ) ;
#60200=CARTESIAN_POINT ( 'NONE',  ( 5.970710119748616762, 0.2212404501104190957, -1.111240891371765516 ) ) ;
#60225=ORIENTED_EDGE ( 'NONE', *, *, #36667, .F. ) ;
#60229=CARTESIAN_POINT ( 'NONE',  ( 4.715620154312000878, -1.320023218807999887, -0.6740770609419000081 ) ) ;
#60349=CARTESIAN_POINT ( 'NONE',  ( 6.356846742204999678, 0.002905985354530999862, 1.468509142934999900 ) ) ;
#60398=LINE ( 'NONE', #23337, #60150 ) ;
#60504=AXIS2_PLACEMENT_3D ( 'NONE', #50308, #28647, #61821 ) ;
#60533=EDGE_CURVE ( 'NONE', #47471, #2054, #13787, .T. ) ;
#60544=CARTESIAN_POINT ( 'NONE',  ( 5.792965594767167659, -1.015451808980873949, 0.5038350337957896441 ) ) ;
#60580=( LENGTH_UNIT ( ) NAMED_UNIT ( * ) SI_UNIT ( .MILLI., .METRE. ) );
#60601=CARTESIAN_POINT ( 'NONE',  ( 6.125178865300000552, -1.528745275297999973, -0.5198780721924000092 ) ) ;
#60669=EDGE_LOOP ( 'NONE', ( #14305, #10587 ) ) ;
#60691=CARTESIAN_POINT ( 'NONE',  ( 6.832448840113999999, -0.8351886993729999986, 1.025064727650000007 ) ) ;
#60700=CARTESIAN_POINT ( 'NONE',  ( -0.2999999999999999889, 0.5773502691895999739, -1.000000000000000000 ) ) ;
#60710=CARTESIAN_POINT ( 'NONE',  ( 5.452606837613999780, -0.4199405305951999789, 1.440017343911000003 ) ) ;
#60726=CARTESIAN_POINT ( 'NONE',  ( 6.013359839683499075, -1.310679582531389276, 0.7554284705563443225 ) ) ;
#60744=CARTESIAN_POINT ( 'NONE',  ( 0.7000000000000000666, 1.154700538379000108, 0.000000000000000000 ) ) ;
#60891=CARTESIAN_POINT ( 'NONE',  ( 0.2000000000000000389, 2.149999999999999911, 0.000000000000000000 ) ) ;
#60912=CARTESIAN_POINT ( 'NONE',  ( 0.2000000000000000389, 0.000000000000000000, 0.000000000000000000 ) ) ;
#60948=CARTESIAN_POINT ( 'NONE',  ( 5.145433571222000069, -1.346921469446999975, 0.5851709088685000948 ) ) ;
#60957=PLANE ( 'NONE',  #63387 ) ;
#61011=CARTESIAN_POINT ( 'NONE',  ( -0.2999999999999999889, -0.5773502691895999739, 1.000000000000000000 ) ) ;
#61029=EDGE_CURVE ( 'NONE', #40878, #68681, #24648, .T. ) ;
#61041=CARTESIAN_POINT ( 'NONE',  ( 6.501421824151000450, 0.7188269793800999841, -0.9308427218166001049 ) ) ;
#61048=AXIS2_PLACEMENT_3D ( 'NONE', #51256, #56847, #67657 ) ;
#61175=CARTESIAN_POINT ( 'NONE',  ( 1.700000000000000178, 2.149999999999999911, 0.000000000000000000 ) ) ;
#61197=ORIENTED_EDGE ( 'NONE', *, *, #55402, .F. ) ;
#61206=COLOUR_RGB ( '', 0.09019608, 0.27058824, 0.51372549) ;
#61298=VECTOR ( 'NONE', #37286, 1000.000000000000000 ) ;
#61307=CARTESIAN_POINT ( 'NONE',  ( 6.670294783753479173, -0.1881139380374373116, -1.513300629325556201 ) ) ;
#61359=ORIENTED_EDGE ( 'NONE', *, *, #14327, .F. ) ;
#61385=CARTESIAN_POINT ( 'NONE',  ( 6.602250463385000323, 1.103230901197000069, 0.4075104821199000416 ) ) ;
#61493=ORIENTED_EDGE ( 'NONE', *, *, #67732, .F. ) ;
#61576=CARTESIAN_POINT ( 'NONE',  ( 5.292049206183823351, -1.006254710013267717, 0.5206924512979714814 ) ) ;
#61649=CIRCLE ( 'NONE', #60504, 1.649999999999999911 ) ;
#61720=CARTESIAN_POINT ( 'NONE',  ( 6.076234045860000599, 0.7526323975856999970, -1.087207638099000118 ) ) ;
#61766=AXIS2_PLACEMENT_3D ( 'NONE', #21005, #52468, #32193 ) ;
#61789=AXIS2_PLACEMENT_3D ( 'NONE', #54518, #34514, #24692 ) ;
#61821=DIRECTION ( 'NONE',  ( 0.000000000000000000, -1.000000000000000000, 0.000000000000000000 ) ) ;
#61835=CARTESIAN_POINT ( 'NONE',  ( 6.544609839683332986, -1.500000000000000444, 0.1963495408493560745 ) ) ;
#61860=VECTOR ( 'NONE', #19927, 1000.000000000000114 ) ;
#61874=CARTESIAN_POINT ( 'NONE',  ( 5.391115032920665406, 0.7145727369020858921, 1.339076430445264032 ) ) ;
#61931=AXIS2_PLACEMENT_3D ( 'NONE', #12728, #34058, #1892 ) ;
#61995=CARTESIAN_POINT ( 'NONE',  ( 6.584068549836916695, -1.425304930403541004, -0.5415159910133545695 ) ) ;
#62041=DIRECTION ( 'NONE',  ( 0.000000000000000000, -1.000000000000000000, 0.000000000000000000 ) ) ;
#62066=CARTESIAN_POINT ( 'NONE',  ( 6.025819726242999330, -0.03703453004475999732, -1.321780775251000017 ) ) ;
#62145=VECTOR ( 'NONE', #66876, 1000.000000000000000 ) ;
#62212=VERTEX_POINT ( 'NONE', #1159 ) ;
#62235=CARTESIAN_POINT ( 'NONE',  ( 5.347090849689999814, 0.7718853692621999718, -1.249287881180999982 ) ) ;
#62238=AXIS2_PLACEMENT_3D ( 'NONE', #57082, #20028, #19688 ) ;
#62272=CARTESIAN_POINT ( 'NONE',  ( 6.899999438051000133, 1.266765207443000030, 0.8033093483900000109 ) ) ;
#62305=CARTESIAN_POINT ( 'NONE',  ( -0.2999999999999999889, 0.5773502691895999739, 1.000000000000000000 ) ) ;
#62325=LINE ( 'NONE', #40313, #19451 ) ;
#62360=CARTESIAN_POINT ( 'NONE',  ( 4.400000000000000355, 0.5526513453421999511, 1.394480724316999876 ) ) ;
#62389=CIRCLE ( 'NONE', #67927, 2.149999999999999911 ) ;
#62396=CARTESIAN_POINT ( 'NONE',  ( 6.462873758167999583, 0.02828639361845000297, -1.175746811673999970 ) ) ;
#62489=PLANE ( 'NONE',  #43362 ) ;
#62572=CARTESIAN_POINT ( 'NONE',  ( 6.377250463384999790, 1.514695785805999950, 0.5594970275663000425 ) ) ;
#62653=CARTESIAN_POINT ( 'NONE',  ( 4.661160569768000528, 0.5205051299898000305, 1.007958462633000041 ) ) ;
#62687=ORIENTED_EDGE ( 'NONE', *, *, #63908, .F. ) ;
#62741=PRODUCT_CONTEXT ( 'NONE', #42282, 'mechanical' ) ;
#62803=CARTESIAN_POINT ( 'NONE',  ( 7.193698479222000230, -0.8911225501965001072, 0.9093353740403999907 ) ) ;
#62831=ORIENTED_EDGE ( 'NONE', *, *, #32832, .T. ) ;
#62923=LINE ( 'NONE', #9442, #55532 ) ;
#62941=ORIENTED_EDGE ( 'NONE', *, *, #27244, .F. ) ;
#62984=CARTESIAN_POINT ( 'NONE',  ( 4.284853625320999448, -0.9992745876934998606, 0.5369886066053000118 ) ) ;
#63040=EDGE_LOOP ( 'NONE', ( #6172, #4233, #39817, #49702 ) ) ;
#63107=CARTESIAN_POINT ( 'NONE',  ( 5.034865712291000328, -1.474529322351999960, 0.5016153125228000054 ) ) ;
#63114=AXIS2_PLACEMENT_3D ( 'NONE', #47327, #42076, #31591 ) ;
#63121=CARTESIAN_POINT ( 'NONE',  ( 0.7000000000000000666, 0.000000000000000000, 0.5999999999999999778 ) ) ;
#63132=DIRECTION ( 'NONE',  ( -1.000000000000000000, 0.000000000000000000, 0.000000000000000000 ) ) ;
#63143=CARTESIAN_POINT ( 'NONE',  ( 6.961241552806000321, 1.068399614603999792, -0.6924786331873999945 ) ) ;
#63230=FACE_OUTER_BOUND ( 'NONE', #56261, .T. ) ;
#63277=DIRECTION ( 'NONE',  ( 0.000000000000000000, -1.000000000000000000, 0.000000000000000000 ) ) ;
#63286=EDGE_CURVE ( 'NONE', #6824, #54765, #46447, .T. ) ;
#63331=CARTESIAN_POINT ( 'NONE',  ( 4.626950847545000300, 0.8932343018606000440, 0.6993127588698000441 ) ) ;
#63387=AXIS2_PLACEMENT_3D ( 'NONE', #2232, #44887, #2566 ) ;
#63398=LINE ( 'NONE', #15519, #1320 ) ;
#63436=AXIS2_PLACEMENT_3D ( 'NONE', #31305, #42479, #63443 ) ;
#63443=DIRECTION ( 'NONE',  ( 0.000000000000000000, 1.000000000000000000, 0.000000000000000000 ) ) ;
#63459=CARTESIAN_POINT ( 'NONE',  ( 5.445382378960999858, -0.1840109337218999719, 1.546599278641000108 ) ) ;
#63460=CARTESIAN_POINT ( 'NONE',  ( 5.146693173016833711, -1.310679582531386611, -0.7554284705563495406 ) ) ;
#63468=CARTESIAN_POINT ( 'NONE',  ( 4.400000000000000355, 1.266759534686000110, 0.8033182938792000627 ) ) ;
#63478=EDGE_CURVE ( 'NONE', #11589, #27875, #15584, .T. ) ;
#63493=CARTESIAN_POINT ( 'NONE',  ( 6.861617155770999510, -0.3226229809382999969, -1.231632514461999950 ) ) ;
#63552=CARTESIAN_POINT ( 'NONE',  ( 7.090737316147470715, 0.3434952630163173315, -1.274854790665578941 ) ) ;
#63580=ORIENTED_EDGE ( 'NONE', *, *, #46793, .T. ) ;
#63582=CARTESIAN_POINT ( 'NONE',  ( 7.028203291589999679, 0.2006192615549000080, -1.234405135879000026 ) ) ;
#63585=DIRECTION ( 'NONE',  ( 0.000000000000000000, 0.8445063564576198445, 0.5355455292528128464 ) ) ;
#63602=EDGE_CURVE ( 'NONE', #31811, #52040, #39667, .T. ) ;
#63682=CARTESIAN_POINT ( 'NONE',  ( 4.432228487644000126, -1.190661282979999847, -0.4572756141791000095 ) ) ;
#63748=CARTESIAN_POINT ( 'NONE',  ( 4.721693173016666023, 0.7554284705563509839, -1.310679582531386167 ) ) ;
#63763=CARTESIAN_POINT ( 'NONE',  ( 5.980603783354000669, 1.250196283310000211, -0.4306799594067000081 ) ) ;
#63784=ADVANCED_FACE ( 'NONE', ( #44919 ), #18346, .F. ) ;
#63807=DIRECTION ( 'NONE',  ( -1.000000000000000000, 0.000000000000000000, 0.000000000000000000 ) ) ;
#63823=ORIENTED_EDGE ( 'NONE', *, *, #55402, .T. ) ;
#63836=CARTESIAN_POINT ( 'NONE',  ( 7.226906611567000205, -1.149357487460000105, 0.4566943152281999763 ) ) ;
#63838=VERTEX_POINT ( 'NONE', #26600 ) ;
#63850=CARTESIAN_POINT ( 'NONE',  ( 5.284193173016667799, 1.460959015002474493, -0.3926218265389176953 ) ) ;
#63868=ORIENTED_EDGE ( 'NONE', *, *, #20348, .F. ) ;
#63896=LINE ( 'NONE', #16011, #50101 ) ;
#63908=EDGE_CURVE ( 'NONE', #426, #58024, #68437, .T. ) ;
#63922=CARTESIAN_POINT ( 'NONE',  ( 6.961914452361000372, 0.1816583604578000111, -1.117739201043999930 ) ) ;
#63950=CARTESIAN_POINT ( 'NONE',  ( 5.605026506349999771, -1.500000000000000000, 0.000000000000000000 ) ) ;
#63981=DIRECTION ( 'NONE',  ( 0.000000000000000000, 0.000000000000000000, 1.000000000000000000 ) ) ;
#64018=CARTESIAN_POINT ( 'NONE',  ( 4.797999458657999483, -1.073975598522000086, 0.3653522499201999896 ) ) ;
#64029=CARTESIAN_POINT ( 'NONE',  ( 4.771693173016333667, 0.7554284705563509839, -1.310679582531385945 ) ) ;
#64033=ORIENTED_EDGE ( 'NONE', *, *, #68351, .F. ) ;
#64054=ORIENTED_EDGE ( 'NONE', *, *, #59112, .F. ) ;
#64069=FACE_OUTER_BOUND ( 'NONE', #16517, .T. ) ;
#64070=CARTESIAN_POINT ( 'NONE',  ( 4.604558767843999867, 1.154756044014000116, 0.2749155220972999691 ) ) ;
#64088=CARTESIAN_POINT ( 'NONE',  ( 4.575859839683333874, -1.460959015002473826, -0.3926218265389207485 ) ) ;
#64103=CARTESIAN_POINT ( 'NONE',  ( 6.081432422588000541, 0.7848946462383999956, 1.064150538460000073 ) ) ;
#64130=CARTESIAN_POINT ( 'NONE',  ( 6.520684977710001107, -0.7452859457610933047, 1.338676382078441307 ) ) ;
#64140=CARTESIAN_POINT ( 'NONE',  ( 6.169609839683334762, -0.1963495408493606265, -1.500000000000000222 ) ) ;
#64145=CARTESIAN_POINT ( 'NONE',  ( 4.487510156732001043, -0.9398597281081001453, 1.241979931278999860 ) ) ;
#64179=CARTESIAN_POINT ( 'NONE',  ( 6.815869870238000061, 0.2268263219687999821, -1.395656501875000011 ) ) ;
#64198=CARTESIAN_POINT ( 'NONE',  ( 7.040773995485999137, -1.461948210420000116, 0.3790019357670000311 ) ) ;
#64205=ORIENTED_EDGE ( 'NONE', *, *, #34615, .T. ) ;
#64288=CARTESIAN_POINT ( 'NONE',  ( 5.688359839683333696, -0.7554284705563480973, -1.310679582531387277 ) ) ;
#64293=ADVANCED_FACE ( 'NONE', ( #41554 ), #42255, .F. ) ;
#64298=CARTESIAN_POINT ( 'NONE',  ( 7.399999875133000060, 0.9999998751120001694, 1.219901821080000081E-10 ) ) ;
#64302=CARTESIAN_POINT ( 'NONE',  ( 5.555026506349999948, -1.500000000000000000, 0.000000000000000000 ) ) ;
#64335=CARTESIAN_POINT ( 'NONE',  ( 5.214996238499456815, -0.1443403793638295407, 1.113928983458401856 ) ) ;
#64383=CARTESIAN_POINT ( 'NONE',  ( 6.778816671981999775, -0.8882170986559999593, 0.6661914818925001036 ) ) ;
#64388=CARTESIAN_POINT ( 'NONE',  ( 6.967819507915497645, 0.1833634693192602583, -1.128230691838603805 ) ) ;
#64409=CARTESIAN_POINT ( 'NONE',  ( 4.902164461081000013, 0.3345035914287000089, -1.292002046660999826 ) ) ;
#64410=AXIS2_PLACEMENT_3D ( 'NONE', #60912, #51113, #3889 ) ;
#64439=CARTESIAN_POINT ( 'NONE',  ( 6.283089701056000287, -1.251891003439999928, -0.4257286625704000405 ) ) ;
#64484=CARTESIAN_POINT ( 'NONE',  ( 5.400636683305999775, -0.7159326393614999784, 1.172178427657000199 ) ) ;
#64503=EDGE_CURVE ( 'NONE', #2358, #58209, #4317, .T. ) ;
#64539=CARTESIAN_POINT ( 'NONE',  ( 5.528344406978000336, -1.481027812490000040, 0.6434334968688999457 ) ) ;
#64562=ORIENTED_EDGE ( 'NONE', *, *, #42947, .T. ) ;
#64608=ORIENTED_EDGE ( 'NONE', *, *, #36667, .T. ) ;
#64610=CARTESIAN_POINT ( 'NONE',  ( 7.293868350350999563, -0.4381732831389000271, 1.171330428861999895 ) ) ;
#64629=ADVANCED_FACE ( 'NONE', ( #43464 ), #32131, .F. ) ;
#64687=CARTESIAN_POINT ( 'NONE',  ( 5.227606837614000135, -0.3108367803229999948, 1.065889863396000115 ) ) ;
#64729=CARTESIAN_POINT ( 'NONE',  ( 6.520102287872433067, 0.8301889199828892396, -0.7704547082435005967 ) ) ;
#64757=CARTESIAN_POINT ( 'NONE',  ( 5.092181265428000536, -0.6485384500295999777, 1.210768222740999933 ) ) ;
#64771=CARTESIAN_POINT ( 'NONE',  ( 5.938359839683334584, 0.7554284705563453217, 1.310679582531389276 ) ) ;
#64784=LINE ( 'NONE', #16897, #44211 ) ;
#64789=CARTESIAN_POINT ( 'NONE',  ( 5.678117865652999363, -0.7240778834237999728, 1.106429931180000104 ) ) ;
#64825=CARTESIAN_POINT ( 'NONE',  ( 6.200859839683334762, 0.3926218265389221362, -1.460959015002473160 ) ) ;
#64831=CARTESIAN_POINT ( 'NONE',  ( 5.298007516638000070, 0.9565531964925000352, 1.044714011268000009 ) ) ;
#64885=CARTESIAN_POINT ( 'NONE',  ( 5.701460587185000151, 1.361663118425000096, -0.5499102030850999689 ) ) ;
#64947=CARTESIAN_POINT ( 'NONE',  ( 6.994995159244999705, -0.3168999327563999935, -1.209784435933999980 ) ) ;
#64981=CYLINDRICAL_SURFACE ( 'NONE', #66085, 2.149999999999999911 ) ;
#64988=CARTESIAN_POINT ( 'NONE',  ( 5.763359839684166985, 1.310679582531388387, -0.7554284705563470981 ) ) ;
#65036=CARTESIAN_POINT ( 'NONE',  ( 7.199141827028999963, 0.000000000000000000, 0.000000000000000000 ) ) ;
#65071=CARTESIAN_POINT ( 'NONE',  ( 5.502110917525607547, 0.6366072631350736533, -0.9373824548834209791 ) ) ;
#65102=CARTESIAN_POINT ( 'NONE',  ( 5.034914323403000047, 0.9510812144104999755, -0.7102707857375000211 ) ) ;
#65110=FILL_AREA_STYLE ('',( #22820 ) ) ;
#65135=CARTESIAN_POINT ( 'NONE',  ( 6.585575618757999905, 0.7284491026353999699, 1.103547660897999938 ) ) ;
#65180=CARTESIAN_POINT ( 'NONE',  ( 5.024329738858000383, -1.220804671313000078, -0.7183737188287999675 ) ) ;
#65238=CARTESIAN_POINT ( 'NONE',  ( 6.889531036634999772, 0.8895447933473999980, 1.347595971237000256 ) ) ;
#65284=CARTESIAN_POINT ( 'NONE',  ( 6.617301518455933618, -1.500125606900863939, -0.2316530497092380014 ) ) ;
#65340=ADVANCED_FACE ( 'NONE', ( #66754 ), #51364, .F. ) ;
#65360=ORIENTED_EDGE ( 'NONE', *, *, #37605, .F. ) ;
#65375=FACE_OUTER_BOUND ( 'NONE', #53810, .T. ) ;
#65417=CARTESIAN_POINT ( 'NONE',  ( 4.646693173015832734, -1.310679582531386611, -0.7554284705563495406 ) ) ;
#65429=CARTESIAN_POINT ( 'NONE',  ( 6.358516356071935327, -1.061705381105392032, -0.3968015536708104918 ) ) ;
#65458=CARTESIAN_POINT ( 'NONE',  ( 4.955958905525999825, 1.069320748165000001, -0.7985724841332999535 ) ) ;
#65474=AXIS2_PLACEMENT_3D ( 'NONE', #39741, #19090, #66291 ) ;
#65488=CARTESIAN_POINT ( 'NONE',  ( 6.074764545683000172, -1.539848055637000002, 0.4860074956841999860 ) ) ;
#65585=VERTEX_POINT ( 'NONE', #23336 ) ;
#65586=CARTESIAN_POINT ( 'NONE',  ( 5.444320540949000531, -0.1571859003484000206, 1.535560374452000110 ) ) ;
#65599=EDGE_LOOP ( 'NONE', ( #23073, #18807 ) ) ;
#65623=VERTEX_POINT ( 'NONE', #55844 ) ;
#65687=DIRECTION ( 'NONE',  ( 0.000000000000000000, -1.000000000000000000, 0.000000000000000000 ) ) ;
#65775=CARTESIAN_POINT ( 'NONE',  ( 6.067661678829444405, 1.119639795224268930, -0.1760443708165491672 ) ) ;
#65804=CARTESIAN_POINT ( 'NONE',  ( 4.690459180880000467, -0.6685019426975999934, -1.486331215039000009 ) ) ;
#65811=( NAMED_UNIT ( * ) SI_UNIT ( $, .STERADIAN. ) SOLID_ANGLE_UNIT ( ) );
#65927=CARTESIAN_POINT ( 'NONE',  ( 6.882863159730999492, -1.197190821580000009, 0.3103650564550000102 ) ) ;
#65960=CARTESIAN_POINT ( 'NONE',  ( 7.156776345353000224, 1.243223188895000053, 2.274921040069000118E-10 ) ) ;
#65970=CARTESIAN_POINT ( 'NONE',  ( 6.850806999420246512, 1.515637746885903470, -0.07806395800591044154 ) ) ;
#66041=CARTESIAN_POINT ( 'NONE',  ( 6.555026506349999948, -1.500000000000000000, 0.000000000000000000 ) ) ;
#66085=AXIS2_PLACEMENT_3D ( 'NONE', #47637, #54512, #68948 ) ;
#66095=DIRECTION ( 'NONE',  ( 1.000000000000000000, 0.000000000000000000, 0.000000000000000000 ) ) ;
#66124=CARTESIAN_POINT ( 'NONE',  ( 5.405159358444773687, -0.6598885925774604644, -0.9208617643536302078 ) ) ;
#66139=CARTESIAN_POINT ( 'NONE',  ( -0.2999999999999999889, -1.154700538379000108, 0.000000000000000000 ) ) ;
#66151=CARTESIAN_POINT ( 'NONE',  ( 0.7000000000000000666, -0.5773502691895999739, -1.000000000000000000 ) ) ;
#66183=CARTESIAN_POINT ( 'NONE',  ( 5.397505169306999306, 1.361663118425000096, -0.5499102030850999689 ) ) ;
#66275=CARTESIAN_POINT ( 'NONE',  ( 6.429134283178000508, -1.251891003439999928, -0.4257286625704000405 ) ) ;
#66291=DIRECTION ( 'NONE',  ( 0.000000000000000000, -1.000000000000000000, 0.000000000000000000 ) ) ;
#66319=CARTESIAN_POINT ( 'NONE',  ( 6.887676285888210792, 1.390704803993308092, 0.6075771062923210897 ) ) ;
#66348=EDGE_CURVE ( 'NONE', #25719, #6927, #56343, .T. ) ;
#66378=ORIENTED_EDGE ( 'NONE', *, *, #54837, .F. ) ;
#66441=CARTESIAN_POINT ( 'NONE',  ( 1.700000000000000178, 0.000000000000000000, 0.000000000000000000 ) ) ;
#66450=ORIENTED_EDGE ( 'NONE', *, *, #34465, .F. ) ;
#66478=CARTESIAN_POINT ( 'NONE',  ( 5.520886616771333522, -1.393043258182025346, 0.6426200619446648110 ) ) ;
#66528=VECTOR ( 'NONE', #50792, 1000.000000000000114 ) ;
#66542=CARTESIAN_POINT ( 'NONE',  ( 6.828376212599681416, 1.461404173720322053, 0.4338462895806718955 ) ) ;
#66602=DIRECTION ( 'NONE',  ( -1.000000000000000000, 0.000000000000000000, 0.000000000000000000 ) ) ;
#66621=CARTESIAN_POINT ( 'NONE',  ( 6.787102968646999912, -1.006517980596000061, 0.5009083264753000364 ) ) ;
#66630=B_SPLINE_CURVE_WITH_KNOTS ( 'NONE', 3,
 ( #23745, #13615, #51007, #18854, #34601, #35280, #55569, #29706, #7319, #3107, #24439, #55914, #50323, #45765, #2421, #28660, #61835, #66041 ),
 .UNSPECIFIED., .F., .F.,
 ( 4, 2, 2, 2, 2, 2, 2, 2, 4 ),
 ( 0.000000000000000000, 0.1249999999999999722, 0.2499999999999999445, 0.3749999999999998890, 0.4999999999999998890, 0.6249999999999998890, 0.7499999999999997780, 0.8749999999999998890, 1.000000000000000000 ),
 .UNSPECIFIED. ) ;
#66633=CARTESIAN_POINT ( 'NONE',  ( 3.400000000000000355, -1.500000000000000000, 0.000000000000000000 ) ) ;
#66643=VERTEX_POINT ( 'NONE', #29485 ) ;
#66646=CARTESIAN_POINT ( 'NONE',  ( 5.594609839683376329, -1.500000000000000888, 0.1963495408493559080 ) ) ;
#66656=EDGE_CURVE ( 'NONE', #36346, #6237, #40631, .T. ) ;
#66659=ORIENTED_EDGE ( 'NONE', *, *, #43879, .F. ) ;
#66739=FACE_OUTER_BOUND ( 'NONE', #34981, .T. ) ;
#66754=FACE_OUTER_BOUND ( 'NONE', #51727, .T. ) ;
#66842=DIRECTION ( 'NONE',  ( 1.000000000000000000, 0.000000000000000000, 0.000000000000000000 ) ) ;
#66876=DIRECTION ( 'NONE',  ( 1.000000000000000000, 0.000000000000000000, 0.000000000000000000 ) ) ;
#66959=ADVANCED_FACE ( 'NONE', ( #49315 ), #43078, .T. ) ;
#66964=CARTESIAN_POINT ( 'NONE',  ( 5.975405406625999838, -0.8123280412348000690, -1.043359539020999982 ) ) ;
#66992=CARTESIAN_POINT ( 'NONE',  ( 3.400000000000000355, 0.000000000000000000, 0.000000000000000000 ) ) ;
#67053=DIRECTION ( 'NONE',  ( 1.000000000000000000, 0.000000000000000000, 0.000000000000000000 ) ) ;
#67260=EDGE_CURVE ( 'NONE', #41499, #49026, #34548, .T. ) ;
#67292=ADVANCED_FACE ( 'NONE', ( #23326 ), #28579, .T. ) ;
#67300=CARTESIAN_POINT ( 'NONE',  ( 6.630791561646000254, 1.270915225504000157, -0.3650349355777000038 ) ) ;
#67347=EDGE_CURVE ( 'NONE', #34817, #25079, #27851, .T. ) ;
#67471=CARTESIAN_POINT ( 'NONE',  ( 4.982454287316000929, -0.1571859003484000206, 1.535560374452000110 ) ) ;
#67522=LINE ( 'NONE', #67867, #51869 ) ;
#67571=VERTEX_POINT ( 'NONE', #32925 ) ;
#67657=DIRECTION ( 'NONE',  ( 0.000000000000000000, 1.000000000000000000, 0.000000000000000000 ) ) ;
#67715=CARTESIAN_POINT ( 'NONE',  ( 5.159193173016666911, -0.3926218265389189721, -1.460959015002473604 ) ) ;
#67721=ORIENTED_EDGE ( 'NONE', *, *, #27450, .T. ) ;
#67732=EDGE_CURVE ( 'NONE', #42702, #44271, #54591, .T. ) ;
#67761=AXIS2_PLACEMENT_3D ( 'NONE', #18953, #66842, #13030 ) ;
#67793=CARTESIAN_POINT ( 'NONE',  ( 6.994740308324000289, -1.394461760113000048, 0.5163436683935999083 ) ) ;
#67812=CARTESIAN_POINT ( 'NONE',  ( 5.195847890838999561, -1.431922326323000094, -0.3257311615064000243 ) ) ;
#67824=( GEOMETRIC_REPRESENTATION_CONTEXT ( 3 ) GLOBAL_UNCERTAINTY_ASSIGNED_CONTEXT ( ( #13405 ) ) GLOBAL_UNIT_ASSIGNED_CONTEXT ( ( #59088, #11190, #38455 ) ) REPRESENTATION_CONTEXT ( 'NONE', 'WORKASPACE' ) );
#67867=CARTESIAN_POINT ( 'NONE',  ( 7.199141827028999963, 0.000000000000000000, -1.200857723089999940 ) ) ;
#67898=CARTESIAN_POINT ( 'NONE',  ( 4.238373395050000880, 0.5984951807791000222, 1.096724531692999882 ) ) ;
#67900=CIRCLE ( 'NONE', #55644, 2.149999999999999911 ) ;
#67927=AXIS2_PLACEMENT_3D ( 'NONE', #2889, #24213, #45556 ) ;
#67944=EDGE_CURVE ( 'NONE', #3150, #36346, #53398, .T. ) ;
#67978=CARTESIAN_POINT ( 'NONE',  ( 6.815773995485999492, -1.064812127159999955, 0.2760466167989999997 ) ) ;
#68017=CARTESIAN_POINT ( 'NONE',  ( 5.125859839683417185, -1.460959015002473382, -0.3926218265389205819 ) ) ;
#68050=CARTESIAN_POINT ( 'NONE',  ( 6.869746981740999736, 1.502678685822000038, 0.3990061803045000244 ) ) ;
#68072=ORIENTED_EDGE ( 'NONE', *, *, #56098, .F. ) ;
#68124=CARTESIAN_POINT ( 'NONE',  ( 7.289711015751999312, -0.9708250560305000665, 0.5387387265405000347 ) ) ;
#68234=CARTESIAN_POINT ( 'NONE',  ( 5.208516125328000790, -0.1340246339512000118, 1.126467857079999968 ) ) ;
#68252=ORIENTED_EDGE ( 'NONE', *, *, #34615, .F. ) ;
#68351=EDGE_CURVE ( 'NONE', #44271, #37125, #22750, .T. ) ;
#68388=CARTESIAN_POINT ( 'NONE',  ( 7.114743061344000807, -0.9896579195269999962, 1.009884616012000080 ) ) ;
#68394=CARTESIAN_POINT ( 'NONE',  ( 6.899999438051000133, 0.5526611926744998682, 1.394476821647000042 ) ) ;
#68437=CIRCLE ( 'NONE', #61766, 1.500000000000000000 ) ;
#68448=CARTESIAN_POINT ( 'NONE',  ( -0.2999999999999999889, -0.5773502691895999739, -1.000000000000000000 ) ) ;
#68494=ORIENTED_EDGE ( 'NONE', *, *, #36137, .F. ) ;
#68532=CARTESIAN_POINT ( 'NONE',  ( 7.127331191709949998, -0.2622596576204692664, 1.265536610600155099 ) ) ;
#68577=CARTESIAN_POINT ( 'NONE',  ( 5.184842376537999620, 1.175001787988000146, 0.4961318581031999297 ) ) ;
#68592=FACE_BOUND ( 'NONE', #51608, .T. ) ;
#68620=DIRECTION ( 'NONE',  ( 0.000000000000000000, 0.000000000000000000, 1.000000000000000000 ) ) ;
#68647=CARTESIAN_POINT ( 'NONE',  ( 4.400000000000000355, 1.266759534686000110, 0.8033182938792000627 ) ) ;
#68648=CARTESIAN_POINT ( 'NONE',  ( 4.607109839683332986, -1.199500263597270244, -0.9218200799623728070 ) ) ;
#68662=CARTESIAN_POINT ( 'NONE',  ( 6.412459438551000090, -0.6732323296109999911, -0.9643333493903999409 ) ) ;
#68681=VERTEX_POINT ( 'NONE', #5667 ) ;
#68689=VERTEX_POINT ( 'NONE', #43079 ) ;
#68738=CARTESIAN_POINT ( 'NONE',  ( 6.803330717051000676, 1.304674974472000093, -0.8456194954836000477 ) ) ;
#68763=CARTESIAN_POINT ( 'NONE',  ( 6.219609839683335473, -0.1963495408493605987, -1.500000000000000444 ) ) ;
#68764=ORIENTED_EDGE ( 'NONE', *, *, #49497, .F. ) ;
#68822=EDGE_LOOP ( 'NONE', ( #12424, #2968, #40716, #20195 ) ) ;
#68853=CARTESIAN_POINT ( 'NONE',  ( 5.771693173016667622, 0.7554284705563509839, -1.310679582531385945 ) ) ;
#68866=ORIENTED_EDGE ( 'NONE', *, *, #56041, .T. ) ;
#68906=CARTESIAN_POINT ( 'NONE',  ( 4.921193962081806816, -0.4916051705834446062, -1.093023166939333990 ) ) ;
#68914=CARTESIAN_POINT ( 'NONE',  ( 1.700000000000000178, 0.000000000000000000, 0.000000000000000000 ) ) ;
#68931=CARTESIAN_POINT ( 'NONE',  ( 4.911164598758000821, -1.268823648606999921, -0.1298529817190000046 ) ) ;
#68948=DIRECTION ( 'NONE',  ( 0.000000000000000000, -1.000000000000000000, 0.000000000000000000 ) ) ;
#68991=AXIS2_PLACEMENT_3D ( 'NONE', #44730, #3091, #65687 ) ;
#68999=CARTESIAN_POINT ( 'NONE',  ( 4.399663372146739526, 1.348965324306665048, -0.3595321560971826425 ) ) ;
#69013=CARTESIAN_POINT ( 'NONE',  ( 6.355377242029001117, 0.8975578082598999474, -1.162289642979999815 ) ) ;
#69019=B_SPLINE_CURVE_WITH_KNOTS ( 'NONE', 3,
 ( #7598, #65284, #33489, #28237, #49553, #1665, #28947, #28593, #50251, #2353, #49904, #23335, #44676, #23676, #65970, #45014, #66319, #18442 ),
 .UNSPECIFIED., .F., .F.,
 ( 4, 2, 2, 2, 2, 2, 2, 2, 4 ),
 ( 0.000000000000000000, 0.1250000000000000000, 0.2500000000000000000, 0.3750000000000000000, 0.5000000000000000000, 0.6250000000000000000, 0.7500000000000000000, 0.8750000000000000000, 1.000000000000000000 ),
 .UNSPECIFIED. ) ;
#69054=LINE ( 'NONE', #11692, #60121 ) ;
#69091=CARTESIAN_POINT ( 'NONE',  ( 6.807740044269000812, -1.061937232448999957, 0.3932159216488000375 ) ) ;
#69122=ORIENTED_EDGE ( 'NONE', *, *, #7617, .F. ) ;
#69125=CIRCLE ( 'NONE', #12038, 1.500000000000000444 ) ;
#69172=CARTESIAN_POINT ( 'NONE',  ( 7.393365321925000622, -0.9580424575664999720, 0.9776229950699999449 ) ) ;
#69178=CARTESIAN_POINT ( 'NONE',  ( 6.976638848880287291, -1.323261473620580553, 0.6079296519753562000 ) ) ;
ENDSEC;
END-ISO-10303-21;
